ISO-10303-21;
HEADER;
/* Generated by software containing ST-Developer
 * from STEP Tools, Inc. (www.steptools.com) 
 */

FILE_DESCRIPTION(
/* description */ (''),
/* implementation_level */ '2;1');

FILE_NAME(
/* name */ 'Bottom_Block.step',
/* time_stamp */ '2026-10-23T17:00:58+06:00',
/* author */ (''),
/* organization */ (''),
/* preprocessor_version */ 'ST-DEVELOPER v20.2',
/* originating_system */ 'Autodesk Translation Framework v15.15.0.0',
/* authorisation */ '');

FILE_SCHEMA (('AUTOMOTIVE_DESIGN { 1 0 10303 214 3 1 1 }'));
ENDSEC;

DATA;
#10=MECHANICAL_DESIGN_GEOMETRIC_PRESENTATION_REPRESENTATION('',(#110),#11385);
#64=SPHERICAL_SURFACE('',#5818,3.);
#65=SPHERICAL_SURFACE('',#5844,3.);
#66=SPHERICAL_SURFACE('',#5846,3.);
#84=SHAPE_REPRESENTATION_RELATIONSHIP('SRR','None',#11436,#97);
#97=ADVANCED_BREP_SHAPE_REPRESENTATION('',(#123),#11376);
#110=STYLED_ITEM('',(#11546),#123);
#123=MANIFOLD_SOLID_BREP('Bottom_Block',#5346);
#153=FACE_BOUND('',#1127,.T.);
#154=FACE_BOUND('',#1128,.T.);
#155=FACE_BOUND('',#1129,.T.);
#156=FACE_BOUND('',#1130,.T.);
#157=FACE_BOUND('',#1131,.T.);
#158=FACE_BOUND('',#1132,.T.);
#159=FACE_BOUND('',#1133,.T.);
#160=FACE_BOUND('',#1134,.T.);
#161=FACE_BOUND('',#1147,.T.);
#162=FACE_BOUND('',#1148,.T.);
#163=FACE_BOUND('',#1149,.T.);
#164=FACE_BOUND('',#1150,.T.);
#165=FACE_BOUND('',#1151,.T.);
#227=CONICAL_SURFACE('',#5848,1.5,0.785398163397448);
#228=CONICAL_SURFACE('',#5852,1.5,0.785398163397448);
#229=CONICAL_SURFACE('',#5856,1.5,0.785398163397448);
#230=CONICAL_SURFACE('',#5860,1.5,0.785398163397448);
#231=CONICAL_SURFACE('',#5864,1.5,0.785398163397448);
#232=CONICAL_SURFACE('',#5886,1.5,0.785398163397448);
#233=CONICAL_SURFACE('',#5887,1.5,0.785398163397448);
#234=CONICAL_SURFACE('',#5888,1.5,0.785398163397448);
#235=CONICAL_SURFACE('',#5890,0.75,0.785398163397447);
#236=CONICAL_SURFACE('',#5893,0.750000000000001,0.785398163397446);
#237=CONICAL_SURFACE('',#5896,0.75,0.785398163397448);
#238=CONICAL_SURFACE('',#5899,2.25,0.785398163397446);
#239=CONICAL_SURFACE('',#5901,0.75,0.785398163397448);
#240=CONICAL_SURFACE('',#5904,0.750000000000001,0.785398163397446);
#241=CONICAL_SURFACE('',#5907,0.749999999999999,0.78539816339745);
#242=CONICAL_SURFACE('',#5910,0.750000000000001,0.785398163397447);
#243=CONICAL_SURFACE('',#5912,2.25,0.785398163397446);
#244=CONICAL_SURFACE('',#5915,0.75,0.785398163397448);
#245=CONICAL_SURFACE('',#5918,0.750000000000001,0.785398163397446);
#246=CONICAL_SURFACE('',#5921,0.75,0.785398163397447);
#247=CONICAL_SURFACE('',#5924,0.749999999999999,0.785398163397449);
#248=CONICAL_SURFACE('',#5927,3.75,0.785398163397447);
#249=CONICAL_SURFACE('',#5930,0.75,0.785398163397448);
#250=CONICAL_SURFACE('',#5954,0.75,0.785398163397447);
#251=CONICAL_SURFACE('',#5956,0.750000000000001,0.785398163397446);
#252=CONICAL_SURFACE('',#5958,0.75,0.785398163397448);
#253=CONICAL_SURFACE('',#5960,2.25,0.785398163397446);
#254=CONICAL_SURFACE('',#5961,0.75,0.785398163397448);
#255=CONICAL_SURFACE('',#5963,0.750000000000001,0.785398163397446);
#256=CONICAL_SURFACE('',#5965,0.749999999999999,0.78539816339745);
#257=CONICAL_SURFACE('',#5967,0.750000000000001,0.785398163397447);
#258=CONICAL_SURFACE('',#5969,2.25,0.785398163397446);
#259=CONICAL_SURFACE('',#5972,0.75,0.785398163397448);
#260=CONICAL_SURFACE('',#5975,0.750000000000001,0.785398163397446);
#261=CONICAL_SURFACE('',#5978,0.75,0.785398163397447);
#262=CONICAL_SURFACE('',#5981,0.749999999999999,0.785398163397449);
#263=CONICAL_SURFACE('',#5984,3.75,0.785398163397447);
#264=CONICAL_SURFACE('',#5987,0.75,0.785398163397448);
#413=CIRCLE('',#5819,2.59807621135332);
#414=CIRCLE('',#5820,3.);
#415=CIRCLE('',#5822,0.5);
#416=CIRCLE('',#5823,3.5);
#417=CIRCLE('',#5824,0.499999999999998);
#418=CIRCLE('',#5825,0.500000000000001);
#419=CIRCLE('',#5826,0.500000000000002);
#420=CIRCLE('',#5827,0.5);
#421=CIRCLE('',#5828,2.5);
#422=CIRCLE('',#5829,0.500000000000001);
#423=CIRCLE('',#5830,0.499999999999998);
#424=CIRCLE('',#5831,0.500000000000002);
#425=CIRCLE('',#5832,0.5);
#426=CIRCLE('',#5833,2.5);
#427=CIRCLE('',#5834,0.5);
#428=CIRCLE('',#5835,0.500000000000002);
#429=CIRCLE('',#5836,0.500000000000001);
#430=CIRCLE('',#5837,1.75);
#431=CIRCLE('',#5838,1.75);
#432=CIRCLE('',#5839,6.);
#433=CIRCLE('',#5840,1.75);
#434=CIRCLE('',#5841,1.75);
#435=CIRCLE('',#5842,2.59807621135332);
#436=CIRCLE('',#5843,2.59807621135332);
#437=CIRCLE('',#5845,3.);
#438=CIRCLE('',#5847,3.);
#439=CIRCLE('',#5849,1.25);
#440=CIRCLE('',#5851,1.25);
#441=CIRCLE('',#5853,1.25);
#442=CIRCLE('',#5855,1.25);
#443=CIRCLE('',#5857,1.25);
#444=CIRCLE('',#5859,1.25);
#445=CIRCLE('',#5861,1.25);
#446=CIRCLE('',#5863,1.25);
#447=CIRCLE('',#5865,1.75);
#448=CIRCLE('',#5867,0.500000000000001);
#449=CIRCLE('',#5868,0.500000000000002);
#450=CIRCLE('',#5869,0.5);
#451=CIRCLE('',#5870,2.5);
#452=CIRCLE('',#5871,0.5);
#453=CIRCLE('',#5872,0.500000000000002);
#454=CIRCLE('',#5873,0.499999999999998);
#455=CIRCLE('',#5874,0.500000000000001);
#456=CIRCLE('',#5875,2.5);
#457=CIRCLE('',#5876,0.5);
#458=CIRCLE('',#5877,0.500000000000002);
#459=CIRCLE('',#5878,0.500000000000001);
#460=CIRCLE('',#5879,0.499999999999998);
#461=CIRCLE('',#5880,3.5);
#462=CIRCLE('',#5881,0.5);
#463=CIRCLE('',#5882,1.75);
#464=CIRCLE('',#5883,1.75);
#465=CIRCLE('',#5884,6.);
#466=CIRCLE('',#5885,1.75);
#467=CIRCLE('',#5891,1.);
#468=CIRCLE('',#5894,1.);
#469=CIRCLE('',#5897,1.);
#470=CIRCLE('',#5900,2.);
#471=CIRCLE('',#5902,1.);
#472=CIRCLE('',#5905,1.);
#473=CIRCLE('',#5908,1.);
#474=CIRCLE('',#5911,1.);
#475=CIRCLE('',#5913,2.);
#476=CIRCLE('',#5916,1.);
#477=CIRCLE('',#5919,1.);
#478=CIRCLE('',#5922,1.);
#479=CIRCLE('',#5925,1.);
#480=CIRCLE('',#5928,4.);
#481=CIRCLE('',#5931,1.);
#482=CIRCLE('',#5934,1.);
#483=CIRCLE('',#5937,1.);
#484=CIRCLE('',#5940,1.);
#485=CIRCLE('',#5942,2.);
#486=CIRCLE('',#5945,1.);
#487=CIRCLE('',#5948,1.);
#488=CIRCLE('',#5951,1.);
#489=CIRCLE('',#5968,1.);
#490=CIRCLE('',#5970,2.);
#491=CIRCLE('',#5973,1.);
#492=CIRCLE('',#5976,1.);
#493=CIRCLE('',#5979,1.);
#494=CIRCLE('',#5982,1.);
#495=CIRCLE('',#5985,4.);
#496=CIRCLE('',#5988,1.);
#579=CYLINDRICAL_SURFACE('',#5850,1.25);
#580=CYLINDRICAL_SURFACE('',#5854,1.25);
#581=CYLINDRICAL_SURFACE('',#5858,1.25);
#582=CYLINDRICAL_SURFACE('',#5862,1.25);
#583=CYLINDRICAL_SURFACE('',#5933,1.);
#584=CYLINDRICAL_SURFACE('',#5936,1.);
#585=CYLINDRICAL_SURFACE('',#5939,1.);
#586=CYLINDRICAL_SURFACE('',#5941,2.);
#587=CYLINDRICAL_SURFACE('',#5944,1.);
#588=CYLINDRICAL_SURFACE('',#5947,1.);
#589=CYLINDRICAL_SURFACE('',#5950,1.);
#590=CYLINDRICAL_SURFACE('',#5989,2.);
#591=CYLINDRICAL_SURFACE('',#5991,1.);
#592=CYLINDRICAL_SURFACE('',#5993,1.);
#593=CYLINDRICAL_SURFACE('',#5995,1.);
#594=CYLINDRICAL_SURFACE('',#5997,1.);
#595=CYLINDRICAL_SURFACE('',#5999,4.);
#596=CYLINDRICAL_SURFACE('',#6001,1.);
#597=CYLINDRICAL_SURFACE('',#6002,1.);
#598=CYLINDRICAL_SURFACE('',#6003,6.);
#778=FACE_OUTER_BOUND('',#1125,.T.);
#779=FACE_OUTER_BOUND('',#1126,.T.);
#780=FACE_OUTER_BOUND('',#1135,.T.);
#781=FACE_OUTER_BOUND('',#1136,.T.);
#782=FACE_OUTER_BOUND('',#1137,.T.);
#783=FACE_OUTER_BOUND('',#1138,.T.);
#784=FACE_OUTER_BOUND('',#1139,.T.);
#785=FACE_OUTER_BOUND('',#1140,.T.);
#786=FACE_OUTER_BOUND('',#1141,.T.);
#787=FACE_OUTER_BOUND('',#1142,.T.);
#788=FACE_OUTER_BOUND('',#1143,.T.);
#789=FACE_OUTER_BOUND('',#1144,.T.);
#790=FACE_OUTER_BOUND('',#1145,.T.);
#791=FACE_OUTER_BOUND('',#1146,.T.);
#792=FACE_OUTER_BOUND('',#1152,.T.);
#793=FACE_OUTER_BOUND('',#1153,.T.);
#794=FACE_OUTER_BOUND('',#1154,.T.);
#795=FACE_OUTER_BOUND('',#1155,.T.);
#796=FACE_OUTER_BOUND('',#1156,.T.);
#797=FACE_OUTER_BOUND('',#1157,.T.);
#798=FACE_OUTER_BOUND('',#1158,.T.);
#799=FACE_OUTER_BOUND('',#1159,.T.);
#800=FACE_OUTER_BOUND('',#1160,.T.);
#801=FACE_OUTER_BOUND('',#1161,.T.);
#802=FACE_OUTER_BOUND('',#1162,.T.);
#803=FACE_OUTER_BOUND('',#1163,.T.);
#804=FACE_OUTER_BOUND('',#1164,.T.);
#805=FACE_OUTER_BOUND('',#1165,.T.);
#806=FACE_OUTER_BOUND('',#1166,.T.);
#807=FACE_OUTER_BOUND('',#1167,.T.);
#808=FACE_OUTER_BOUND('',#1168,.T.);
#809=FACE_OUTER_BOUND('',#1169,.T.);
#810=FACE_OUTER_BOUND('',#1170,.T.);
#811=FACE_OUTER_BOUND('',#1171,.T.);
#812=FACE_OUTER_BOUND('',#1172,.T.);
#813=FACE_OUTER_BOUND('',#1173,.T.);
#814=FACE_OUTER_BOUND('',#1174,.T.);
#815=FACE_OUTER_BOUND('',#1175,.T.);
#816=FACE_OUTER_BOUND('',#1176,.T.);
#817=FACE_OUTER_BOUND('',#1177,.T.);
#818=FACE_OUTER_BOUND('',#1178,.T.);
#819=FACE_OUTER_BOUND('',#1179,.T.);
#820=FACE_OUTER_BOUND('',#1180,.T.);
#821=FACE_OUTER_BOUND('',#1181,.T.);
#822=FACE_OUTER_BOUND('',#1182,.T.);
#823=FACE_OUTER_BOUND('',#1183,.T.);
#824=FACE_OUTER_BOUND('',#1184,.T.);
#825=FACE_OUTER_BOUND('',#1185,.T.);
#826=FACE_OUTER_BOUND('',#1186,.T.);
#827=FACE_OUTER_BOUND('',#1187,.T.);
#828=FACE_OUTER_BOUND('',#1188,.T.);
#829=FACE_OUTER_BOUND('',#1189,.T.);
#830=FACE_OUTER_BOUND('',#1190,.T.);
#831=FACE_OUTER_BOUND('',#1191,.T.);
#832=FACE_OUTER_BOUND('',#1192,.T.);
#833=FACE_OUTER_BOUND('',#1193,.T.);
#834=FACE_OUTER_BOUND('',#1194,.T.);
#835=FACE_OUTER_BOUND('',#1195,.T.);
#836=FACE_OUTER_BOUND('',#1196,.T.);
#837=FACE_OUTER_BOUND('',#1197,.T.);
#838=FACE_OUTER_BOUND('',#1198,.T.);
#839=FACE_OUTER_BOUND('',#1199,.T.);
#840=FACE_OUTER_BOUND('',#1200,.T.);
#841=FACE_OUTER_BOUND('',#1201,.T.);
#842=FACE_OUTER_BOUND('',#1202,.T.);
#843=FACE_OUTER_BOUND('',#1203,.T.);
#844=FACE_OUTER_BOUND('',#1204,.T.);
#845=FACE_OUTER_BOUND('',#1205,.T.);
#846=FACE_OUTER_BOUND('',#1206,.T.);
#847=FACE_OUTER_BOUND('',#1207,.T.);
#848=FACE_OUTER_BOUND('',#1208,.T.);
#849=FACE_OUTER_BOUND('',#1209,.T.);
#850=FACE_OUTER_BOUND('',#1210,.T.);
#851=FACE_OUTER_BOUND('',#1211,.T.);
#852=FACE_OUTER_BOUND('',#1212,.T.);
#853=FACE_OUTER_BOUND('',#1213,.T.);
#854=FACE_OUTER_BOUND('',#1214,.T.);
#855=FACE_OUTER_BOUND('',#1215,.T.);
#856=FACE_OUTER_BOUND('',#1216,.T.);
#857=FACE_OUTER_BOUND('',#1217,.T.);
#858=FACE_OUTER_BOUND('',#1218,.T.);
#859=FACE_OUTER_BOUND('',#1219,.T.);
#860=FACE_OUTER_BOUND('',#1220,.T.);
#861=FACE_OUTER_BOUND('',#1221,.T.);
#862=FACE_OUTER_BOUND('',#1222,.T.);
#863=FACE_OUTER_BOUND('',#1223,.T.);
#864=FACE_OUTER_BOUND('',#1224,.T.);
#865=FACE_OUTER_BOUND('',#1225,.T.);
#866=FACE_OUTER_BOUND('',#1226,.T.);
#867=FACE_OUTER_BOUND('',#1227,.T.);
#868=FACE_OUTER_BOUND('',#1228,.T.);
#869=FACE_OUTER_BOUND('',#1229,.T.);
#870=FACE_OUTER_BOUND('',#1230,.T.);
#871=FACE_OUTER_BOUND('',#1231,.T.);
#872=FACE_OUTER_BOUND('',#1232,.T.);
#873=FACE_OUTER_BOUND('',#1233,.T.);
#874=FACE_OUTER_BOUND('',#1234,.T.);
#875=FACE_OUTER_BOUND('',#1235,.T.);
#876=FACE_OUTER_BOUND('',#1236,.T.);
#877=FACE_OUTER_BOUND('',#1237,.T.);
#878=FACE_OUTER_BOUND('',#1238,.T.);
#879=FACE_OUTER_BOUND('',#1239,.T.);
#1125=EDGE_LOOP('',(#4214,#4215,#4216));
#1126=EDGE_LOOP('',(#4217,#4218,#4219,#4220,#4221,#4222,#4223,#4224,#4225,
#4226,#4227,#4228,#4229,#4230,#4231,#4232,#4233,#4234,#4235,#4236,#4237,
#4238,#4239,#4240,#4241,#4242,#4243,#4244));
#1127=EDGE_LOOP('',(#4245));
#1128=EDGE_LOOP('',(#4246));
#1129=EDGE_LOOP('',(#4247));
#1130=EDGE_LOOP('',(#4248));
#1131=EDGE_LOOP('',(#4249));
#1132=EDGE_LOOP('',(#4250));
#1133=EDGE_LOOP('',(#4251));
#1134=EDGE_LOOP('',(#4252));
#1135=EDGE_LOOP('',(#4253,#4254,#4255));
#1136=EDGE_LOOP('',(#4256,#4257,#4258));
#1137=EDGE_LOOP('',(#4259,#4260,#4261,#4262));
#1138=EDGE_LOOP('',(#4263,#4264,#4265,#4266));
#1139=EDGE_LOOP('',(#4267,#4268,#4269,#4270));
#1140=EDGE_LOOP('',(#4271,#4272,#4273,#4274));
#1141=EDGE_LOOP('',(#4275,#4276,#4277,#4278));
#1142=EDGE_LOOP('',(#4279,#4280,#4281,#4282));
#1143=EDGE_LOOP('',(#4283,#4284,#4285,#4286));
#1144=EDGE_LOOP('',(#4287,#4288,#4289,#4290));
#1145=EDGE_LOOP('',(#4291,#4292,#4293,#4294));
#1146=EDGE_LOOP('',(#4295,#4296,#4297,#4298,#4299,#4300,#4301,#4302,#4303,
#4304,#4305,#4306,#4307,#4308,#4309,#4310,#4311,#4312,#4313,#4314,#4315,
#4316,#4317,#4318,#4319,#4320,#4321,#4322));
#1147=EDGE_LOOP('',(#4323));
#1148=EDGE_LOOP('',(#4324));
#1149=EDGE_LOOP('',(#4325));
#1150=EDGE_LOOP('',(#4326));
#1151=EDGE_LOOP('',(#4327));
#1152=EDGE_LOOP('',(#4328,#4329,#4330,#4331));
#1153=EDGE_LOOP('',(#4332,#4333,#4334,#4335));
#1154=EDGE_LOOP('',(#4336,#4337,#4338,#4339));
#1155=EDGE_LOOP('',(#4340,#4341,#4342,#4343));
#1156=EDGE_LOOP('',(#4344,#4345,#4346,#4347));
#1157=EDGE_LOOP('',(#4348,#4349,#4350,#4351));
#1158=EDGE_LOOP('',(#4352,#4353,#4354,#4355));
#1159=EDGE_LOOP('',(#4356,#4357,#4358,#4359));
#1160=EDGE_LOOP('',(#4360,#4361,#4362,#4363));
#1161=EDGE_LOOP('',(#4364,#4365,#4366,#4367));
#1162=EDGE_LOOP('',(#4368,#4369,#4370,#4371));
#1163=EDGE_LOOP('',(#4372,#4373,#4374,#4375));
#1164=EDGE_LOOP('',(#4376,#4377,#4378,#4379));
#1165=EDGE_LOOP('',(#4380,#4381,#4382,#4383));
#1166=EDGE_LOOP('',(#4384,#4385,#4386,#4387));
#1167=EDGE_LOOP('',(#4388,#4389,#4390,#4391));
#1168=EDGE_LOOP('',(#4392,#4393,#4394,#4395));
#1169=EDGE_LOOP('',(#4396,#4397,#4398,#4399));
#1170=EDGE_LOOP('',(#4400,#4401,#4402,#4403));
#1171=EDGE_LOOP('',(#4404,#4405,#4406,#4407));
#1172=EDGE_LOOP('',(#4408,#4409,#4410,#4411));
#1173=EDGE_LOOP('',(#4412,#4413,#4414,#4415));
#1174=EDGE_LOOP('',(#4416,#4417,#4418,#4419));
#1175=EDGE_LOOP('',(#4420,#4421,#4422,#4423));
#1176=EDGE_LOOP('',(#4424,#4425,#4426,#4427));
#1177=EDGE_LOOP('',(#4428,#4429,#4430,#4431));
#1178=EDGE_LOOP('',(#4432,#4433,#4434,#4435));
#1179=EDGE_LOOP('',(#4436,#4437,#4438,#4439));
#1180=EDGE_LOOP('',(#4440,#4441,#4442,#4443));
#1181=EDGE_LOOP('',(#4444,#4445,#4446,#4447));
#1182=EDGE_LOOP('',(#4448,#4449,#4450,#4451));
#1183=EDGE_LOOP('',(#4452,#4453,#4454,#4455));
#1184=EDGE_LOOP('',(#4456,#4457,#4458,#4459));
#1185=EDGE_LOOP('',(#4460,#4461,#4462,#4463));
#1186=EDGE_LOOP('',(#4464,#4465,#4466,#4467));
#1187=EDGE_LOOP('',(#4468,#4469,#4470,#4471));
#1188=EDGE_LOOP('',(#4472,#4473,#4474,#4475));
#1189=EDGE_LOOP('',(#4476,#4477,#4478,#4479));
#1190=EDGE_LOOP('',(#4480,#4481,#4482,#4483));
#1191=EDGE_LOOP('',(#4484,#4485,#4486,#4487));
#1192=EDGE_LOOP('',(#4488,#4489,#4490,#4491));
#1193=EDGE_LOOP('',(#4492,#4493,#4494,#4495));
#1194=EDGE_LOOP('',(#4496,#4497,#4498,#4499));
#1195=EDGE_LOOP('',(#4500,#4501,#4502,#4503));
#1196=EDGE_LOOP('',(#4504,#4505,#4506,#4507));
#1197=EDGE_LOOP('',(#4508,#4509,#4510,#4511));
#1198=EDGE_LOOP('',(#4512,#4513,#4514,#4515));
#1199=EDGE_LOOP('',(#4516,#4517,#4518,#4519));
#1200=EDGE_LOOP('',(#4520,#4521,#4522,#4523));
#1201=EDGE_LOOP('',(#4524,#4525,#4526,#4527));
#1202=EDGE_LOOP('',(#4528,#4529,#4530,#4531));
#1203=EDGE_LOOP('',(#4532,#4533,#4534,#4535));
#1204=EDGE_LOOP('',(#4536,#4537,#4538,#4539));
#1205=EDGE_LOOP('',(#4540,#4541,#4542,#4543));
#1206=EDGE_LOOP('',(#4544,#4545,#4546,#4547));
#1207=EDGE_LOOP('',(#4548,#4549,#4550,#4551));
#1208=EDGE_LOOP('',(#4552,#4553,#4554,#4555));
#1209=EDGE_LOOP('',(#4556,#4557,#4558,#4559));
#1210=EDGE_LOOP('',(#4560,#4561,#4562,#4563));
#1211=EDGE_LOOP('',(#4564,#4565,#4566,#4567));
#1212=EDGE_LOOP('',(#4568,#4569,#4570,#4571));
#1213=EDGE_LOOP('',(#4572,#4573,#4574,#4575));
#1214=EDGE_LOOP('',(#4576,#4577,#4578,#4579));
#1215=EDGE_LOOP('',(#4580,#4581,#4582,#4583));
#1216=EDGE_LOOP('',(#4584,#4585,#4586,#4587));
#1217=EDGE_LOOP('',(#4588,#4589,#4590,#4591));
#1218=EDGE_LOOP('',(#4592,#4593,#4594,#4595));
#1219=EDGE_LOOP('',(#4596,#4597,#4598,#4599));
#1220=EDGE_LOOP('',(#4600,#4601,#4602,#4603));
#1221=EDGE_LOOP('',(#4604,#4605,#4606,#4607));
#1222=EDGE_LOOP('',(#4608,#4609,#4610,#4611));
#1223=EDGE_LOOP('',(#4612,#4613,#4614,#4615));
#1224=EDGE_LOOP('',(#4616,#4617,#4618,#4619));
#1225=EDGE_LOOP('',(#4620,#4621,#4622,#4623));
#1226=EDGE_LOOP('',(#4624,#4625,#4626,#4627));
#1227=EDGE_LOOP('',(#4628,#4629,#4630,#4631));
#1228=EDGE_LOOP('',(#4632,#4633,#4634,#4635));
#1229=EDGE_LOOP('',(#4636,#4637,#4638,#4639));
#1230=EDGE_LOOP('',(#4640,#4641,#4642,#4643));
#1231=EDGE_LOOP('',(#4644,#4645,#4646,#4647));
#1232=EDGE_LOOP('',(#4648,#4649,#4650,#4651));
#1233=EDGE_LOOP('',(#4652,#4653,#4654,#4655));
#1234=EDGE_LOOP('',(#4656,#4657,#4658,#4659));
#1235=EDGE_LOOP('',(#4660,#4661,#4662,#4663));
#1236=EDGE_LOOP('',(#4664,#4665,#4666,#4667));
#1237=EDGE_LOOP('',(#4668,#4669,#4670,#4671));
#1238=EDGE_LOOP('',(#4672,#4673,#4674,#4675));
#1239=EDGE_LOOP('',(#4676,#4677,#4678,#4679));
#1561=LINE('',#9177,#2023);
#1562=LINE('',#9181,#2024);
#1563=LINE('',#9185,#2025);
#1564=LINE('',#9189,#2026);
#1565=LINE('',#9193,#2027);
#1566=LINE('',#9197,#2028);
#1567=LINE('',#9201,#2029);
#1568=LINE('',#9207,#2030);
#1569=LINE('',#9211,#2031);
#1570=LINE('',#9215,#2032);
#1571=LINE('',#9221,#2033);
#1572=LINE('',#9225,#2034);
#1573=LINE('',#9229,#2035);
#1574=LINE('',#9253,#2036);
#1575=LINE('',#9258,#2037);
#1576=LINE('',#9261,#2038);
#1577=LINE('',#9266,#2039);
#1578=LINE('',#9270,#2040);
#1579=LINE('',#9274,#2041);
#1580=LINE('',#9278,#2042);
#1581=LINE('',#9282,#2043);
#1582=LINE('',#9285,#2044);
#1583=LINE('',#9290,#2045);
#1584=LINE('',#9294,#2046);
#1585=LINE('',#9298,#2047);
#1586=LINE('',#9302,#2048);
#1587=LINE('',#9308,#2049);
#1588=LINE('',#9312,#2050);
#1589=LINE('',#9316,#2051);
#1590=LINE('',#9322,#2052);
#1591=LINE('',#9326,#2053);
#1592=LINE('',#9330,#2054);
#1593=LINE('',#9334,#2055);
#1594=LINE('',#9338,#2056);
#1595=LINE('',#9342,#2057);
#1596=LINE('',#9353,#2058);
#1597=LINE('',#9355,#2059);
#1598=LINE('',#9357,#2060);
#1599=LINE('',#9360,#2061);
#1600=LINE('',#9362,#2062);
#1601=LINE('',#9363,#2063);
#1602=LINE('',#9367,#2064);
#1603=LINE('',#9370,#2065);
#1604=LINE('',#9371,#2066);
#1605=LINE('',#9375,#2067);
#1606=LINE('',#9378,#2068);
#1607=LINE('',#9379,#2069);
#1608=LINE('',#9383,#2070);
#1609=LINE('',#9386,#2071);
#1610=LINE('',#9387,#2072);
#1611=LINE('',#9390,#2073);
#1612=LINE('',#9395,#2074);
#1613=LINE('',#9398,#2075);
#1614=LINE('',#9399,#2076);
#1615=LINE('',#9403,#2077);
#1616=LINE('',#9406,#2078);
#1617=LINE('',#9407,#2079);
#1618=LINE('',#9411,#2080);
#1619=LINE('',#9414,#2081);
#1620=LINE('',#9415,#2082);
#1621=LINE('',#9419,#2083);
#1622=LINE('',#9423,#2084);
#1623=LINE('',#9426,#2085);
#1624=LINE('',#9427,#2086);
#1625=LINE('',#9431,#2087);
#1626=LINE('',#9434,#2088);
#1627=LINE('',#9435,#2089);
#1628=LINE('',#9439,#2090);
#1629=LINE('',#9442,#2091);
#1630=LINE('',#9443,#2092);
#1631=LINE('',#9447,#2093);
#1632=LINE('',#9450,#2094);
#1633=LINE('',#9451,#2095);
#1634=LINE('',#9455,#2096);
#1635=LINE('',#9458,#2097);
#1636=LINE('',#9459,#2098);
#1637=LINE('',#9463,#2099);
#1638=LINE('',#9466,#2100);
#1639=LINE('',#9467,#2101);
#1640=LINE('',#9472,#2102);
#1641=LINE('',#9474,#2103);
#1642=LINE('',#9475,#2104);
#1643=LINE('',#9478,#2105);
#1644=LINE('',#9482,#2106);
#1645=LINE('',#9483,#2107);
#1646=LINE('',#9486,#2108);
#1647=LINE('',#9490,#2109);
#1648=LINE('',#9491,#2110);
#1649=LINE('',#9494,#2111);
#1650=LINE('',#9498,#2112);
#1651=LINE('',#9502,#2113);
#1652=LINE('',#9503,#2114);
#1653=LINE('',#9506,#2115);
#1654=LINE('',#9510,#2116);
#1655=LINE('',#9511,#2117);
#1656=LINE('',#9514,#2118);
#1657=LINE('',#9518,#2119);
#1658=LINE('',#9519,#2120);
#1659=LINE('',#9522,#2121);
#1660=LINE('',#9526,#2122);
#1661=LINE('',#9527,#2123);
#1662=LINE('',#9529,#2124);
#1663=LINE('',#9530,#2125);
#1664=LINE('',#9532,#2126);
#1665=LINE('',#9534,#2127);
#1666=LINE('',#9536,#2128);
#1667=LINE('',#9538,#2129);
#1668=LINE('',#9540,#2130);
#1669=LINE('',#9542,#2131);
#1670=LINE('',#9544,#2132);
#1671=LINE('',#9546,#2133);
#1672=LINE('',#9548,#2134);
#1673=LINE('',#9550,#2135);
#1674=LINE('',#9552,#2136);
#1675=LINE('',#9554,#2137);
#1676=LINE('',#9556,#2138);
#1677=LINE('',#9559,#2139);
#1678=LINE('',#9563,#2140);
#1679=LINE('',#9567,#2141);
#1680=LINE('',#9568,#2142);
#1681=LINE('',#9571,#2143);
#1682=LINE('',#9575,#2144);
#1683=LINE('',#9576,#2145);
#1684=LINE('',#9579,#2146);
#1685=LINE('',#9583,#2147);
#1686=LINE('',#9584,#2148);
#1687=LINE('',#9587,#2149);
#1688=LINE('',#9591,#2150);
#1689=LINE('',#9592,#2151);
#1690=LINE('',#9595,#2152);
#1691=LINE('',#9599,#2153);
#1692=LINE('',#9600,#2154);
#1693=LINE('',#9603,#2155);
#1694=LINE('',#9607,#2156);
#1695=LINE('',#9608,#2157);
#1696=LINE('',#9612,#2158);
#1697=LINE('',#9613,#2159);
#1698=LINE('',#9615,#2160);
#1699=LINE('',#9617,#2161);
#1700=LINE('',#9619,#2162);
#1701=LINE('',#9621,#2163);
#1702=LINE('',#9623,#2164);
#1703=LINE('',#9625,#2165);
#1704=LINE('',#9627,#2166);
#1705=LINE('',#9629,#2167);
#1706=LINE('',#9631,#2168);
#1707=LINE('',#9633,#2169);
#1708=LINE('',#9635,#2170);
#1709=LINE('',#9639,#2171);
#2023=VECTOR('',#7020,10.);
#2024=VECTOR('',#7023,10.);
#2025=VECTOR('',#7026,10.);
#2026=VECTOR('',#7029,10.);
#2027=VECTOR('',#7032,10.);
#2028=VECTOR('',#7035,10.);
#2029=VECTOR('',#7038,10.);
#2030=VECTOR('',#7043,10.);
#2031=VECTOR('',#7046,10.);
#2032=VECTOR('',#7049,10.);
#2033=VECTOR('',#7054,10.);
#2034=VECTOR('',#7057,10.);
#2035=VECTOR('',#7060,10.);
#2036=VECTOR('',#7087,1.5);
#2037=VECTOR('',#7094,1.25);
#2038=VECTOR('',#7097,1.5);
#2039=VECTOR('',#7104,1.25);
#2040=VECTOR('',#7109,1.5);
#2041=VECTOR('',#7114,1.25);
#2042=VECTOR('',#7119,1.5);
#2043=VECTOR('',#7124,1.25);
#2044=VECTOR('',#7127,1.5);
#2045=VECTOR('',#7132,10.);
#2046=VECTOR('',#7135,10.);
#2047=VECTOR('',#7138,10.);
#2048=VECTOR('',#7141,10.);
#2049=VECTOR('',#7146,10.);
#2050=VECTOR('',#7149,10.);
#2051=VECTOR('',#7152,10.);
#2052=VECTOR('',#7157,10.);
#2053=VECTOR('',#7160,10.);
#2054=VECTOR('',#7163,10.);
#2055=VECTOR('',#7166,10.);
#2056=VECTOR('',#7169,10.);
#2057=VECTOR('',#7172,10.);
#2058=VECTOR('',#7185,1.5);
#2059=VECTOR('',#7188,1.5);
#2060=VECTOR('',#7191,1.5);
#2061=VECTOR('',#7194,10.);
#2062=VECTOR('',#7195,10.);
#2063=VECTOR('',#7196,10.);
#2064=VECTOR('',#7201,10.);
#2065=VECTOR('',#7204,10.);
#2066=VECTOR('',#7205,10.);
#2067=VECTOR('',#7210,10.);
#2068=VECTOR('',#7213,10.);
#2069=VECTOR('',#7214,10.);
#2070=VECTOR('',#7219,10.);
#2071=VECTOR('',#7222,10.);
#2072=VECTOR('',#7223,10.);
#2073=VECTOR('',#7226,10.);
#2074=VECTOR('',#7233,10.);
#2075=VECTOR('',#7236,10.);
#2076=VECTOR('',#7237,10.);
#2077=VECTOR('',#7242,10.);
#2078=VECTOR('',#7245,10.);
#2079=VECTOR('',#7246,10.);
#2080=VECTOR('',#7251,10.);
#2081=VECTOR('',#7254,10.);
#2082=VECTOR('',#7255,10.);
#2083=VECTOR('',#7260,10.);
#2084=VECTOR('',#7265,10.);
#2085=VECTOR('',#7268,10.);
#2086=VECTOR('',#7269,10.);
#2087=VECTOR('',#7274,10.);
#2088=VECTOR('',#7277,10.);
#2089=VECTOR('',#7278,10.);
#2090=VECTOR('',#7283,10.);
#2091=VECTOR('',#7286,10.);
#2092=VECTOR('',#7287,10.);
#2093=VECTOR('',#7292,10.);
#2094=VECTOR('',#7295,10.);
#2095=VECTOR('',#7296,10.);
#2096=VECTOR('',#7301,10.);
#2097=VECTOR('',#7304,10.);
#2098=VECTOR('',#7305,10.);
#2099=VECTOR('',#7310,10.);
#2100=VECTOR('',#7313,10.);
#2101=VECTOR('',#7314,10.);
#2102=VECTOR('',#7321,10.);
#2103=VECTOR('',#7322,10.);
#2104=VECTOR('',#7323,10.);
#2105=VECTOR('',#7326,10.);
#2106=VECTOR('',#7331,10.);
#2107=VECTOR('',#7332,10.);
#2108=VECTOR('',#7335,10.);
#2109=VECTOR('',#7340,10.);
#2110=VECTOR('',#7341,10.);
#2111=VECTOR('',#7344,10.);
#2112=VECTOR('',#7349,10.);
#2113=VECTOR('',#7354,10.);
#2114=VECTOR('',#7355,10.);
#2115=VECTOR('',#7358,10.);
#2116=VECTOR('',#7363,10.);
#2117=VECTOR('',#7364,10.);
#2118=VECTOR('',#7367,10.);
#2119=VECTOR('',#7372,10.);
#2120=VECTOR('',#7373,10.);
#2121=VECTOR('',#7376,10.);
#2122=VECTOR('',#7381,10.);
#2123=VECTOR('',#7382,10.);
#2124=VECTOR('',#7385,10.);
#2125=VECTOR('',#7386,10.);
#2126=VECTOR('',#7389,10.);
#2127=VECTOR('',#7392,10.);
#2128=VECTOR('',#7395,10.);
#2129=VECTOR('',#7398,10.);
#2130=VECTOR('',#7401,10.);
#2131=VECTOR('',#7404,10.);
#2132=VECTOR('',#7407,10.);
#2133=VECTOR('',#7410,10.);
#2134=VECTOR('',#7413,10.);
#2135=VECTOR('',#7416,10.);
#2136=VECTOR('',#7419,10.);
#2137=VECTOR('',#7422,10.);
#2138=VECTOR('',#7425,10.);
#2139=VECTOR('',#7428,10.);
#2140=VECTOR('',#7433,10.);
#2141=VECTOR('',#7438,10.);
#2142=VECTOR('',#7439,10.);
#2143=VECTOR('',#7442,10.);
#2144=VECTOR('',#7447,10.);
#2145=VECTOR('',#7448,10.);
#2146=VECTOR('',#7451,10.);
#2147=VECTOR('',#7456,10.);
#2148=VECTOR('',#7457,10.);
#2149=VECTOR('',#7460,10.);
#2150=VECTOR('',#7465,10.);
#2151=VECTOR('',#7466,10.);
#2152=VECTOR('',#7469,10.);
#2153=VECTOR('',#7474,10.);
#2154=VECTOR('',#7475,10.);
#2155=VECTOR('',#7478,10.);
#2156=VECTOR('',#7483,10.);
#2157=VECTOR('',#7484,10.);
#2158=VECTOR('',#7491,10.);
#2159=VECTOR('',#7492,10.);
#2160=VECTOR('',#7495,10.);
#2161=VECTOR('',#7498,10.);
#2162=VECTOR('',#7501,10.);
#2163=VECTOR('',#7504,10.);
#2164=VECTOR('',#7507,10.);
#2165=VECTOR('',#7510,10.);
#2166=VECTOR('',#7513,10.);
#2167=VECTOR('',#7516,10.);
#2168=VECTOR('',#7519,10.);
#2169=VECTOR('',#7522,10.);
#2170=VECTOR('',#7525,10.);
#2171=VECTOR('',#7532,6.);
#2468=VERTEX_POINT('',#9170);
#2469=VERTEX_POINT('',#9172);
#2470=VERTEX_POINT('',#9175);
#2471=VERTEX_POINT('',#9176);
#2472=VERTEX_POINT('',#9178);
#2473=VERTEX_POINT('',#9180);
#2474=VERTEX_POINT('',#9182);
#2475=VERTEX_POINT('',#9184);
#2476=VERTEX_POINT('',#9186);
#2477=VERTEX_POINT('',#9188);
#2478=VERTEX_POINT('',#9190);
#2479=VERTEX_POINT('',#9192);
#2480=VERTEX_POINT('',#9194);
#2481=VERTEX_POINT('',#9196);
#2482=VERTEX_POINT('',#9198);
#2483=VERTEX_POINT('',#9200);
#2484=VERTEX_POINT('',#9202);
#2485=VERTEX_POINT('',#9204);
#2486=VERTEX_POINT('',#9206);
#2487=VERTEX_POINT('',#9208);
#2488=VERTEX_POINT('',#9210);
#2489=VERTEX_POINT('',#9212);
#2490=VERTEX_POINT('',#9214);
#2491=VERTEX_POINT('',#9216);
#2492=VERTEX_POINT('',#9218);
#2493=VERTEX_POINT('',#9220);
#2494=VERTEX_POINT('',#9222);
#2495=VERTEX_POINT('',#9224);
#2496=VERTEX_POINT('',#9226);
#2497=VERTEX_POINT('',#9228);
#2498=VERTEX_POINT('',#9231);
#2499=VERTEX_POINT('',#9233);
#2500=VERTEX_POINT('',#9235);
#2501=VERTEX_POINT('',#9237);
#2502=VERTEX_POINT('',#9239);
#2503=VERTEX_POINT('',#9241);
#2504=VERTEX_POINT('',#9243);
#2505=VERTEX_POINT('',#9246);
#2506=VERTEX_POINT('',#9249);
#2507=VERTEX_POINT('',#9252);
#2508=VERTEX_POINT('',#9256);
#2509=VERTEX_POINT('',#9260);
#2510=VERTEX_POINT('',#9264);
#2511=VERTEX_POINT('',#9268);
#2512=VERTEX_POINT('',#9272);
#2513=VERTEX_POINT('',#9276);
#2514=VERTEX_POINT('',#9280);
#2515=VERTEX_POINT('',#9284);
#2516=VERTEX_POINT('',#9288);
#2517=VERTEX_POINT('',#9289);
#2518=VERTEX_POINT('',#9291);
#2519=VERTEX_POINT('',#9293);
#2520=VERTEX_POINT('',#9295);
#2521=VERTEX_POINT('',#9297);
#2522=VERTEX_POINT('',#9299);
#2523=VERTEX_POINT('',#9301);
#2524=VERTEX_POINT('',#9303);
#2525=VERTEX_POINT('',#9305);
#2526=VERTEX_POINT('',#9307);
#2527=VERTEX_POINT('',#9309);
#2528=VERTEX_POINT('',#9311);
#2529=VERTEX_POINT('',#9313);
#2530=VERTEX_POINT('',#9315);
#2531=VERTEX_POINT('',#9317);
#2532=VERTEX_POINT('',#9319);
#2533=VERTEX_POINT('',#9321);
#2534=VERTEX_POINT('',#9323);
#2535=VERTEX_POINT('',#9325);
#2536=VERTEX_POINT('',#9327);
#2537=VERTEX_POINT('',#9329);
#2538=VERTEX_POINT('',#9331);
#2539=VERTEX_POINT('',#9333);
#2540=VERTEX_POINT('',#9335);
#2541=VERTEX_POINT('',#9337);
#2542=VERTEX_POINT('',#9339);
#2543=VERTEX_POINT('',#9341);
#2544=VERTEX_POINT('',#9344);
#2545=VERTEX_POINT('',#9346);
#2546=VERTEX_POINT('',#9348);
#2547=VERTEX_POINT('',#9350);
#2548=VERTEX_POINT('',#9359);
#2549=VERTEX_POINT('',#9361);
#2550=VERTEX_POINT('',#9365);
#2551=VERTEX_POINT('',#9369);
#2552=VERTEX_POINT('',#9373);
#2553=VERTEX_POINT('',#9377);
#2554=VERTEX_POINT('',#9381);
#2555=VERTEX_POINT('',#9385);
#2556=VERTEX_POINT('',#9389);
#2557=VERTEX_POINT('',#9393);
#2558=VERTEX_POINT('',#9397);
#2559=VERTEX_POINT('',#9401);
#2560=VERTEX_POINT('',#9405);
#2561=VERTEX_POINT('',#9409);
#2562=VERTEX_POINT('',#9413);
#2563=VERTEX_POINT('',#9417);
#2564=VERTEX_POINT('',#9421);
#2565=VERTEX_POINT('',#9425);
#2566=VERTEX_POINT('',#9429);
#2567=VERTEX_POINT('',#9433);
#2568=VERTEX_POINT('',#9437);
#2569=VERTEX_POINT('',#9441);
#2570=VERTEX_POINT('',#9445);
#2571=VERTEX_POINT('',#9449);
#2572=VERTEX_POINT('',#9453);
#2573=VERTEX_POINT('',#9457);
#2574=VERTEX_POINT('',#9461);
#2575=VERTEX_POINT('',#9465);
#2576=VERTEX_POINT('',#9471);
#2577=VERTEX_POINT('',#9473);
#2578=VERTEX_POINT('',#9477);
#2579=VERTEX_POINT('',#9481);
#2580=VERTEX_POINT('',#9485);
#2581=VERTEX_POINT('',#9489);
#2582=VERTEX_POINT('',#9493);
#2583=VERTEX_POINT('',#9497);
#2584=VERTEX_POINT('',#9501);
#2585=VERTEX_POINT('',#9505);
#2586=VERTEX_POINT('',#9509);
#2587=VERTEX_POINT('',#9513);
#2588=VERTEX_POINT('',#9517);
#2589=VERTEX_POINT('',#9521);
#2590=VERTEX_POINT('',#9525);
#2591=VERTEX_POINT('',#9558);
#2592=VERTEX_POINT('',#9562);
#2593=VERTEX_POINT('',#9566);
#2594=VERTEX_POINT('',#9570);
#2595=VERTEX_POINT('',#9574);
#2596=VERTEX_POINT('',#9578);
#2597=VERTEX_POINT('',#9582);
#2598=VERTEX_POINT('',#9586);
#2599=VERTEX_POINT('',#9590);
#2600=VERTEX_POINT('',#9594);
#2601=VERTEX_POINT('',#9598);
#2602=VERTEX_POINT('',#9602);
#2603=VERTEX_POINT('',#9606);
#3072=EDGE_CURVE('',#2468,#2468,#413,.T.);
#3073=EDGE_CURVE('',#2468,#2469,#414,.T.);
#3074=EDGE_CURVE('',#2470,#2471,#1561,.T.);
#3075=EDGE_CURVE('',#2472,#2470,#415,.T.);
#3076=EDGE_CURVE('',#2473,#2472,#1562,.T.);
#3077=EDGE_CURVE('',#2474,#2473,#416,.T.);
#3078=EDGE_CURVE('',#2475,#2474,#1563,.T.);
#3079=EDGE_CURVE('',#2476,#2475,#417,.T.);
#3080=EDGE_CURVE('',#2477,#2476,#1564,.T.);
#3081=EDGE_CURVE('',#2478,#2477,#418,.T.);
#3082=EDGE_CURVE('',#2479,#2478,#1565,.T.);
#3083=EDGE_CURVE('',#2480,#2479,#419,.T.);
#3084=EDGE_CURVE('',#2481,#2480,#1566,.T.);
#3085=EDGE_CURVE('',#2482,#2481,#420,.T.);
#3086=EDGE_CURVE('',#2483,#2482,#1567,.T.);
#3087=EDGE_CURVE('',#2484,#2483,#421,.T.);
#3088=EDGE_CURVE('',#2485,#2484,#422,.T.);
#3089=EDGE_CURVE('',#2486,#2485,#1568,.T.);
#3090=EDGE_CURVE('',#2487,#2486,#423,.T.);
#3091=EDGE_CURVE('',#2488,#2487,#1569,.T.);
#3092=EDGE_CURVE('',#2489,#2488,#424,.T.);
#3093=EDGE_CURVE('',#2490,#2489,#1570,.T.);
#3094=EDGE_CURVE('',#2491,#2490,#425,.T.);
#3095=EDGE_CURVE('',#2492,#2491,#426,.T.);
#3096=EDGE_CURVE('',#2493,#2492,#1571,.T.);
#3097=EDGE_CURVE('',#2494,#2493,#427,.T.);
#3098=EDGE_CURVE('',#2495,#2494,#1572,.T.);
#3099=EDGE_CURVE('',#2496,#2495,#428,.T.);
#3100=EDGE_CURVE('',#2497,#2496,#1573,.T.);
#3101=EDGE_CURVE('',#2471,#2497,#429,.T.);
#3102=EDGE_CURVE('',#2498,#2498,#430,.T.);
#3103=EDGE_CURVE('',#2499,#2499,#431,.T.);
#3104=EDGE_CURVE('',#2500,#2500,#432,.T.);
#3105=EDGE_CURVE('',#2501,#2501,#433,.T.);
#3106=EDGE_CURVE('',#2502,#2502,#434,.T.);
#3107=EDGE_CURVE('',#2503,#2503,#435,.T.);
#3108=EDGE_CURVE('',#2504,#2504,#436,.T.);
#3109=EDGE_CURVE('',#2504,#2505,#437,.T.);
#3110=EDGE_CURVE('',#2503,#2506,#438,.T.);
#3111=EDGE_CURVE('',#2502,#2507,#1574,.T.);
#3112=EDGE_CURVE('',#2507,#2507,#439,.T.);
#3113=EDGE_CURVE('',#2508,#2508,#440,.T.);
#3114=EDGE_CURVE('',#2508,#2507,#1575,.T.);
#3115=EDGE_CURVE('',#2498,#2509,#1576,.T.);
#3116=EDGE_CURVE('',#2509,#2509,#441,.T.);
#3117=EDGE_CURVE('',#2510,#2510,#442,.T.);
#3118=EDGE_CURVE('',#2510,#2509,#1577,.T.);
#3119=EDGE_CURVE('',#2511,#2511,#443,.T.);
#3120=EDGE_CURVE('',#2511,#2501,#1578,.T.);
#3121=EDGE_CURVE('',#2512,#2512,#444,.T.);
#3122=EDGE_CURVE('',#2512,#2511,#1579,.T.);
#3123=EDGE_CURVE('',#2513,#2513,#445,.T.);
#3124=EDGE_CURVE('',#2513,#2499,#1580,.T.);
#3125=EDGE_CURVE('',#2514,#2514,#446,.T.);
#3126=EDGE_CURVE('',#2514,#2513,#1581,.T.);
#3127=EDGE_CURVE('',#2508,#2515,#1582,.T.);
#3128=EDGE_CURVE('',#2515,#2515,#447,.T.);
#3129=EDGE_CURVE('',#2516,#2517,#1583,.T.);
#3130=EDGE_CURVE('',#2518,#2516,#448,.T.);
#3131=EDGE_CURVE('',#2519,#2518,#1584,.T.);
#3132=EDGE_CURVE('',#2520,#2519,#449,.T.);
#3133=EDGE_CURVE('',#2521,#2520,#1585,.T.);
#3134=EDGE_CURVE('',#2522,#2521,#450,.T.);
#3135=EDGE_CURVE('',#2523,#2522,#1586,.T.);
#3136=EDGE_CURVE('',#2524,#2523,#451,.T.);
#3137=EDGE_CURVE('',#2525,#2524,#452,.T.);
#3138=EDGE_CURVE('',#2526,#2525,#1587,.T.);
#3139=EDGE_CURVE('',#2527,#2526,#453,.T.);
#3140=EDGE_CURVE('',#2528,#2527,#1588,.T.);
#3141=EDGE_CURVE('',#2529,#2528,#454,.T.);
#3142=EDGE_CURVE('',#2530,#2529,#1589,.T.);
#3143=EDGE_CURVE('',#2531,#2530,#455,.T.);
#3144=EDGE_CURVE('',#2532,#2531,#456,.T.);
#3145=EDGE_CURVE('',#2533,#2532,#1590,.T.);
#3146=EDGE_CURVE('',#2534,#2533,#457,.T.);
#3147=EDGE_CURVE('',#2535,#2534,#1591,.T.);
#3148=EDGE_CURVE('',#2536,#2535,#458,.T.);
#3149=EDGE_CURVE('',#2537,#2536,#1592,.T.);
#3150=EDGE_CURVE('',#2538,#2537,#459,.T.);
#3151=EDGE_CURVE('',#2539,#2538,#1593,.T.);
#3152=EDGE_CURVE('',#2540,#2539,#460,.T.);
#3153=EDGE_CURVE('',#2541,#2540,#1594,.T.);
#3154=EDGE_CURVE('',#2542,#2541,#461,.T.);
#3155=EDGE_CURVE('',#2543,#2542,#1595,.T.);
#3156=EDGE_CURVE('',#2517,#2543,#462,.T.);
#3157=EDGE_CURVE('',#2544,#2544,#463,.T.);
#3158=EDGE_CURVE('',#2545,#2545,#464,.T.);
#3159=EDGE_CURVE('',#2546,#2546,#465,.T.);
#3160=EDGE_CURVE('',#2547,#2547,#466,.T.);
#3161=EDGE_CURVE('',#2510,#2544,#1596,.T.);
#3162=EDGE_CURVE('',#2547,#2512,#1597,.T.);
#3163=EDGE_CURVE('',#2545,#2514,#1598,.T.);
#3164=EDGE_CURVE('',#2548,#2516,#1599,.T.);
#3165=EDGE_CURVE('',#2517,#2549,#1600,.T.);
#3166=EDGE_CURVE('',#2549,#2548,#1601,.T.);
#3167=EDGE_CURVE('',#2548,#2550,#467,.T.);
#3168=EDGE_CURVE('',#2550,#2518,#1602,.T.);
#3169=EDGE_CURVE('',#2551,#2519,#1603,.T.);
#3170=EDGE_CURVE('',#2550,#2551,#1604,.T.);
#3171=EDGE_CURVE('',#2551,#2552,#468,.T.);
#3172=EDGE_CURVE('',#2552,#2520,#1605,.T.);
#3173=EDGE_CURVE('',#2553,#2521,#1606,.T.);
#3174=EDGE_CURVE('',#2552,#2553,#1607,.T.);
#3175=EDGE_CURVE('',#2553,#2554,#469,.T.);
#3176=EDGE_CURVE('',#2554,#2522,#1608,.T.);
#3177=EDGE_CURVE('',#2555,#2523,#1609,.T.);
#3178=EDGE_CURVE('',#2554,#2555,#1610,.T.);
#3179=EDGE_CURVE('',#2556,#2524,#1611,.T.);
#3180=EDGE_CURVE('',#2555,#2556,#470,.T.);
#3181=EDGE_CURVE('',#2556,#2557,#471,.T.);
#3182=EDGE_CURVE('',#2557,#2525,#1612,.T.);
#3183=EDGE_CURVE('',#2558,#2526,#1613,.T.);
#3184=EDGE_CURVE('',#2557,#2558,#1614,.T.);
#3185=EDGE_CURVE('',#2558,#2559,#472,.T.);
#3186=EDGE_CURVE('',#2559,#2527,#1615,.T.);
#3187=EDGE_CURVE('',#2560,#2528,#1616,.T.);
#3188=EDGE_CURVE('',#2559,#2560,#1617,.T.);
#3189=EDGE_CURVE('',#2560,#2561,#473,.T.);
#3190=EDGE_CURVE('',#2561,#2529,#1618,.T.);
#3191=EDGE_CURVE('',#2561,#2562,#1619,.T.);
#3192=EDGE_CURVE('',#2562,#2530,#1620,.T.);
#3193=EDGE_CURVE('',#2562,#2563,#474,.T.);
#3194=EDGE_CURVE('',#2563,#2531,#1621,.T.);
#3195=EDGE_CURVE('',#2563,#2564,#475,.T.);
#3196=EDGE_CURVE('',#2564,#2532,#1622,.T.);
#3197=EDGE_CURVE('',#2564,#2565,#1623,.T.);
#3198=EDGE_CURVE('',#2565,#2533,#1624,.T.);
#3199=EDGE_CURVE('',#2565,#2566,#476,.T.);
#3200=EDGE_CURVE('',#2566,#2534,#1625,.T.);
#3201=EDGE_CURVE('',#2566,#2567,#1626,.T.);
#3202=EDGE_CURVE('',#2567,#2535,#1627,.T.);
#3203=EDGE_CURVE('',#2567,#2568,#477,.T.);
#3204=EDGE_CURVE('',#2568,#2536,#1628,.T.);
#3205=EDGE_CURVE('',#2568,#2569,#1629,.T.);
#3206=EDGE_CURVE('',#2569,#2537,#1630,.T.);
#3207=EDGE_CURVE('',#2569,#2570,#478,.T.);
#3208=EDGE_CURVE('',#2570,#2538,#1631,.T.);
#3209=EDGE_CURVE('',#2570,#2571,#1632,.T.);
#3210=EDGE_CURVE('',#2571,#2539,#1633,.T.);
#3211=EDGE_CURVE('',#2571,#2572,#479,.T.);
#3212=EDGE_CURVE('',#2572,#2540,#1634,.T.);
#3213=EDGE_CURVE('',#2572,#2573,#1635,.T.);
#3214=EDGE_CURVE('',#2573,#2541,#1636,.T.);
#3215=EDGE_CURVE('',#2573,#2574,#480,.T.);
#3216=EDGE_CURVE('',#2574,#2542,#1637,.T.);
#3217=EDGE_CURVE('',#2575,#2543,#1638,.T.);
#3218=EDGE_CURVE('',#2574,#2575,#1639,.T.);
#3219=EDGE_CURVE('',#2575,#2549,#481,.T.);
#3220=EDGE_CURVE('',#2576,#2561,#1640,.T.);
#3221=EDGE_CURVE('',#2577,#2576,#1641,.T.);
#3222=EDGE_CURVE('',#2562,#2577,#1642,.T.);
#3223=EDGE_CURVE('',#2560,#2578,#1643,.T.);
#3224=EDGE_CURVE('',#2576,#2578,#482,.T.);
#3225=EDGE_CURVE('',#2579,#2559,#1644,.T.);
#3226=EDGE_CURVE('',#2578,#2579,#1645,.T.);
#3227=EDGE_CURVE('',#2558,#2580,#1646,.T.);
#3228=EDGE_CURVE('',#2579,#2580,#483,.T.);
#3229=EDGE_CURVE('',#2581,#2557,#1647,.T.);
#3230=EDGE_CURVE('',#2580,#2581,#1648,.T.);
#3231=EDGE_CURVE('',#2556,#2582,#1649,.T.);
#3232=EDGE_CURVE('',#2581,#2582,#484,.T.);
#3233=EDGE_CURVE('',#2583,#2555,#1650,.T.);
#3234=EDGE_CURVE('',#2582,#2583,#485,.T.);
#3235=EDGE_CURVE('',#2584,#2554,#1651,.T.);
#3236=EDGE_CURVE('',#2583,#2584,#1652,.T.);
#3237=EDGE_CURVE('',#2553,#2585,#1653,.T.);
#3238=EDGE_CURVE('',#2584,#2585,#486,.T.);
#3239=EDGE_CURVE('',#2586,#2552,#1654,.T.);
#3240=EDGE_CURVE('',#2585,#2586,#1655,.T.);
#3241=EDGE_CURVE('',#2551,#2587,#1656,.T.);
#3242=EDGE_CURVE('',#2586,#2587,#487,.T.);
#3243=EDGE_CURVE('',#2588,#2550,#1657,.T.);
#3244=EDGE_CURVE('',#2587,#2588,#1658,.T.);
#3245=EDGE_CURVE('',#2548,#2589,#1659,.T.);
#3246=EDGE_CURVE('',#2588,#2589,#488,.T.);
#3247=EDGE_CURVE('',#2590,#2549,#1660,.T.);
#3248=EDGE_CURVE('',#2589,#2590,#1661,.T.);
#3249=EDGE_CURVE('',#2471,#2589,#1662,.T.);
#3250=EDGE_CURVE('',#2590,#2470,#1663,.T.);
#3251=EDGE_CURVE('',#2497,#2588,#1664,.T.);
#3252=EDGE_CURVE('',#2496,#2587,#1665,.T.);
#3253=EDGE_CURVE('',#2495,#2586,#1666,.T.);
#3254=EDGE_CURVE('',#2494,#2585,#1667,.T.);
#3255=EDGE_CURVE('',#2493,#2584,#1668,.T.);
#3256=EDGE_CURVE('',#2492,#2583,#1669,.T.);
#3257=EDGE_CURVE('',#2491,#2582,#1670,.T.);
#3258=EDGE_CURVE('',#2490,#2581,#1671,.T.);
#3259=EDGE_CURVE('',#2489,#2580,#1672,.T.);
#3260=EDGE_CURVE('',#2488,#2579,#1673,.T.);
#3261=EDGE_CURVE('',#2487,#2578,#1674,.T.);
#3262=EDGE_CURVE('',#2486,#2576,#1675,.T.);
#3263=EDGE_CURVE('',#2485,#2577,#1676,.T.);
#3264=EDGE_CURVE('',#2484,#2591,#1677,.T.);
#3265=EDGE_CURVE('',#2591,#2577,#489,.T.);
#3266=EDGE_CURVE('',#2483,#2592,#1678,.T.);
#3267=EDGE_CURVE('',#2592,#2591,#490,.T.);
#3268=EDGE_CURVE('',#2482,#2593,#1679,.T.);
#3269=EDGE_CURVE('',#2593,#2592,#1680,.T.);
#3270=EDGE_CURVE('',#2481,#2594,#1681,.T.);
#3271=EDGE_CURVE('',#2594,#2593,#491,.T.);
#3272=EDGE_CURVE('',#2480,#2595,#1682,.T.);
#3273=EDGE_CURVE('',#2595,#2594,#1683,.T.);
#3274=EDGE_CURVE('',#2479,#2596,#1684,.T.);
#3275=EDGE_CURVE('',#2596,#2595,#492,.T.);
#3276=EDGE_CURVE('',#2478,#2597,#1685,.T.);
#3277=EDGE_CURVE('',#2597,#2596,#1686,.T.);
#3278=EDGE_CURVE('',#2477,#2598,#1687,.T.);
#3279=EDGE_CURVE('',#2598,#2597,#493,.T.);
#3280=EDGE_CURVE('',#2476,#2599,#1688,.T.);
#3281=EDGE_CURVE('',#2599,#2598,#1689,.T.);
#3282=EDGE_CURVE('',#2475,#2600,#1690,.T.);
#3283=EDGE_CURVE('',#2600,#2599,#494,.T.);
#3284=EDGE_CURVE('',#2474,#2601,#1691,.T.);
#3285=EDGE_CURVE('',#2601,#2600,#1692,.T.);
#3286=EDGE_CURVE('',#2473,#2602,#1693,.T.);
#3287=EDGE_CURVE('',#2602,#2601,#495,.T.);
#3288=EDGE_CURVE('',#2472,#2603,#1694,.T.);
#3289=EDGE_CURVE('',#2603,#2602,#1695,.T.);
#3290=EDGE_CURVE('',#2590,#2603,#496,.T.);
#3291=EDGE_CURVE('',#2591,#2563,#1696,.T.);
#3292=EDGE_CURVE('',#2592,#2564,#1697,.T.);
#3293=EDGE_CURVE('',#2565,#2593,#1698,.T.);
#3294=EDGE_CURVE('',#2594,#2566,#1699,.T.);
#3295=EDGE_CURVE('',#2567,#2595,#1700,.T.);
#3296=EDGE_CURVE('',#2596,#2568,#1701,.T.);
#3297=EDGE_CURVE('',#2569,#2597,#1702,.T.);
#3298=EDGE_CURVE('',#2598,#2570,#1703,.T.);
#3299=EDGE_CURVE('',#2571,#2599,#1704,.T.);
#3300=EDGE_CURVE('',#2600,#2572,#1705,.T.);
#3301=EDGE_CURVE('',#2601,#2573,#1706,.T.);
#3302=EDGE_CURVE('',#2602,#2574,#1707,.T.);
#3303=EDGE_CURVE('',#2575,#2603,#1708,.T.);
#3304=EDGE_CURVE('',#2546,#2500,#1709,.T.);
#4214=ORIENTED_EDGE('',*,*,#3072,.F.);
#4215=ORIENTED_EDGE('',*,*,#3073,.T.);
#4216=ORIENTED_EDGE('',*,*,#3073,.F.);
#4217=ORIENTED_EDGE('',*,*,#3074,.F.);
#4218=ORIENTED_EDGE('',*,*,#3075,.F.);
#4219=ORIENTED_EDGE('',*,*,#3076,.F.);
#4220=ORIENTED_EDGE('',*,*,#3077,.F.);
#4221=ORIENTED_EDGE('',*,*,#3078,.F.);
#4222=ORIENTED_EDGE('',*,*,#3079,.F.);
#4223=ORIENTED_EDGE('',*,*,#3080,.F.);
#4224=ORIENTED_EDGE('',*,*,#3081,.F.);
#4225=ORIENTED_EDGE('',*,*,#3082,.F.);
#4226=ORIENTED_EDGE('',*,*,#3083,.F.);
#4227=ORIENTED_EDGE('',*,*,#3084,.F.);
#4228=ORIENTED_EDGE('',*,*,#3085,.F.);
#4229=ORIENTED_EDGE('',*,*,#3086,.F.);
#4230=ORIENTED_EDGE('',*,*,#3087,.F.);
#4231=ORIENTED_EDGE('',*,*,#3088,.F.);
#4232=ORIENTED_EDGE('',*,*,#3089,.F.);
#4233=ORIENTED_EDGE('',*,*,#3090,.F.);
#4234=ORIENTED_EDGE('',*,*,#3091,.F.);
#4235=ORIENTED_EDGE('',*,*,#3092,.F.);
#4236=ORIENTED_EDGE('',*,*,#3093,.F.);
#4237=ORIENTED_EDGE('',*,*,#3094,.F.);
#4238=ORIENTED_EDGE('',*,*,#3095,.F.);
#4239=ORIENTED_EDGE('',*,*,#3096,.F.);
#4240=ORIENTED_EDGE('',*,*,#3097,.F.);
#4241=ORIENTED_EDGE('',*,*,#3098,.F.);
#4242=ORIENTED_EDGE('',*,*,#3099,.F.);
#4243=ORIENTED_EDGE('',*,*,#3100,.F.);
#4244=ORIENTED_EDGE('',*,*,#3101,.F.);
#4245=ORIENTED_EDGE('',*,*,#3102,.F.);
#4246=ORIENTED_EDGE('',*,*,#3103,.F.);
#4247=ORIENTED_EDGE('',*,*,#3104,.T.);
#4248=ORIENTED_EDGE('',*,*,#3105,.F.);
#4249=ORIENTED_EDGE('',*,*,#3106,.F.);
#4250=ORIENTED_EDGE('',*,*,#3107,.T.);
#4251=ORIENTED_EDGE('',*,*,#3108,.T.);
#4252=ORIENTED_EDGE('',*,*,#3072,.T.);
#4253=ORIENTED_EDGE('',*,*,#3108,.F.);
#4254=ORIENTED_EDGE('',*,*,#3109,.T.);
#4255=ORIENTED_EDGE('',*,*,#3109,.F.);
#4256=ORIENTED_EDGE('',*,*,#3107,.F.);
#4257=ORIENTED_EDGE('',*,*,#3110,.T.);
#4258=ORIENTED_EDGE('',*,*,#3110,.F.);
#4259=ORIENTED_EDGE('',*,*,#3106,.T.);
#4260=ORIENTED_EDGE('',*,*,#3111,.T.);
#4261=ORIENTED_EDGE('',*,*,#3112,.T.);
#4262=ORIENTED_EDGE('',*,*,#3111,.F.);
#4263=ORIENTED_EDGE('',*,*,#3113,.F.);
#4264=ORIENTED_EDGE('',*,*,#3114,.T.);
#4265=ORIENTED_EDGE('',*,*,#3112,.F.);
#4266=ORIENTED_EDGE('',*,*,#3114,.F.);
#4267=ORIENTED_EDGE('',*,*,#3102,.T.);
#4268=ORIENTED_EDGE('',*,*,#3115,.T.);
#4269=ORIENTED_EDGE('',*,*,#3116,.T.);
#4270=ORIENTED_EDGE('',*,*,#3115,.F.);
#4271=ORIENTED_EDGE('',*,*,#3117,.F.);
#4272=ORIENTED_EDGE('',*,*,#3118,.T.);
#4273=ORIENTED_EDGE('',*,*,#3116,.F.);
#4274=ORIENTED_EDGE('',*,*,#3118,.F.);
#4275=ORIENTED_EDGE('',*,*,#3119,.T.);
#4276=ORIENTED_EDGE('',*,*,#3120,.T.);
#4277=ORIENTED_EDGE('',*,*,#3105,.T.);
#4278=ORIENTED_EDGE('',*,*,#3120,.F.);
#4279=ORIENTED_EDGE('',*,*,#3121,.F.);
#4280=ORIENTED_EDGE('',*,*,#3122,.T.);
#4281=ORIENTED_EDGE('',*,*,#3119,.F.);
#4282=ORIENTED_EDGE('',*,*,#3122,.F.);
#4283=ORIENTED_EDGE('',*,*,#3123,.T.);
#4284=ORIENTED_EDGE('',*,*,#3124,.T.);
#4285=ORIENTED_EDGE('',*,*,#3103,.T.);
#4286=ORIENTED_EDGE('',*,*,#3124,.F.);
#4287=ORIENTED_EDGE('',*,*,#3125,.F.);
#4288=ORIENTED_EDGE('',*,*,#3126,.T.);
#4289=ORIENTED_EDGE('',*,*,#3123,.F.);
#4290=ORIENTED_EDGE('',*,*,#3126,.F.);
#4291=ORIENTED_EDGE('',*,*,#3113,.T.);
#4292=ORIENTED_EDGE('',*,*,#3127,.T.);
#4293=ORIENTED_EDGE('',*,*,#3128,.T.);
#4294=ORIENTED_EDGE('',*,*,#3127,.F.);
#4295=ORIENTED_EDGE('',*,*,#3129,.F.);
#4296=ORIENTED_EDGE('',*,*,#3130,.F.);
#4297=ORIENTED_EDGE('',*,*,#3131,.F.);
#4298=ORIENTED_EDGE('',*,*,#3132,.F.);
#4299=ORIENTED_EDGE('',*,*,#3133,.F.);
#4300=ORIENTED_EDGE('',*,*,#3134,.F.);
#4301=ORIENTED_EDGE('',*,*,#3135,.F.);
#4302=ORIENTED_EDGE('',*,*,#3136,.F.);
#4303=ORIENTED_EDGE('',*,*,#3137,.F.);
#4304=ORIENTED_EDGE('',*,*,#3138,.F.);
#4305=ORIENTED_EDGE('',*,*,#3139,.F.);
#4306=ORIENTED_EDGE('',*,*,#3140,.F.);
#4307=ORIENTED_EDGE('',*,*,#3141,.F.);
#4308=ORIENTED_EDGE('',*,*,#3142,.F.);
#4309=ORIENTED_EDGE('',*,*,#3143,.F.);
#4310=ORIENTED_EDGE('',*,*,#3144,.F.);
#4311=ORIENTED_EDGE('',*,*,#3145,.F.);
#4312=ORIENTED_EDGE('',*,*,#3146,.F.);
#4313=ORIENTED_EDGE('',*,*,#3147,.F.);
#4314=ORIENTED_EDGE('',*,*,#3148,.F.);
#4315=ORIENTED_EDGE('',*,*,#3149,.F.);
#4316=ORIENTED_EDGE('',*,*,#3150,.F.);
#4317=ORIENTED_EDGE('',*,*,#3151,.F.);
#4318=ORIENTED_EDGE('',*,*,#3152,.F.);
#4319=ORIENTED_EDGE('',*,*,#3153,.F.);
#4320=ORIENTED_EDGE('',*,*,#3154,.F.);
#4321=ORIENTED_EDGE('',*,*,#3155,.F.);
#4322=ORIENTED_EDGE('',*,*,#3156,.F.);
#4323=ORIENTED_EDGE('',*,*,#3157,.F.);
#4324=ORIENTED_EDGE('',*,*,#3158,.F.);
#4325=ORIENTED_EDGE('',*,*,#3159,.T.);
#4326=ORIENTED_EDGE('',*,*,#3160,.F.);
#4327=ORIENTED_EDGE('',*,*,#3128,.F.);
#4328=ORIENTED_EDGE('',*,*,#3117,.T.);
#4329=ORIENTED_EDGE('',*,*,#3161,.T.);
#4330=ORIENTED_EDGE('',*,*,#3157,.T.);
#4331=ORIENTED_EDGE('',*,*,#3161,.F.);
#4332=ORIENTED_EDGE('',*,*,#3160,.T.);
#4333=ORIENTED_EDGE('',*,*,#3162,.T.);
#4334=ORIENTED_EDGE('',*,*,#3121,.T.);
#4335=ORIENTED_EDGE('',*,*,#3162,.F.);
#4336=ORIENTED_EDGE('',*,*,#3158,.T.);
#4337=ORIENTED_EDGE('',*,*,#3163,.T.);
#4338=ORIENTED_EDGE('',*,*,#3125,.T.);
#4339=ORIENTED_EDGE('',*,*,#3163,.F.);
#4340=ORIENTED_EDGE('',*,*,#3164,.T.);
#4341=ORIENTED_EDGE('',*,*,#3129,.T.);
#4342=ORIENTED_EDGE('',*,*,#3165,.T.);
#4343=ORIENTED_EDGE('',*,*,#3166,.T.);
#4344=ORIENTED_EDGE('',*,*,#3164,.F.);
#4345=ORIENTED_EDGE('',*,*,#3167,.T.);
#4346=ORIENTED_EDGE('',*,*,#3168,.T.);
#4347=ORIENTED_EDGE('',*,*,#3130,.T.);
#4348=ORIENTED_EDGE('',*,*,#3169,.T.);
#4349=ORIENTED_EDGE('',*,*,#3131,.T.);
#4350=ORIENTED_EDGE('',*,*,#3168,.F.);
#4351=ORIENTED_EDGE('',*,*,#3170,.T.);
#4352=ORIENTED_EDGE('',*,*,#3169,.F.);
#4353=ORIENTED_EDGE('',*,*,#3171,.T.);
#4354=ORIENTED_EDGE('',*,*,#3172,.T.);
#4355=ORIENTED_EDGE('',*,*,#3132,.T.);
#4356=ORIENTED_EDGE('',*,*,#3173,.T.);
#4357=ORIENTED_EDGE('',*,*,#3133,.T.);
#4358=ORIENTED_EDGE('',*,*,#3172,.F.);
#4359=ORIENTED_EDGE('',*,*,#3174,.T.);
#4360=ORIENTED_EDGE('',*,*,#3173,.F.);
#4361=ORIENTED_EDGE('',*,*,#3175,.T.);
#4362=ORIENTED_EDGE('',*,*,#3176,.T.);
#4363=ORIENTED_EDGE('',*,*,#3134,.T.);
#4364=ORIENTED_EDGE('',*,*,#3177,.T.);
#4365=ORIENTED_EDGE('',*,*,#3135,.T.);
#4366=ORIENTED_EDGE('',*,*,#3176,.F.);
#4367=ORIENTED_EDGE('',*,*,#3178,.T.);
#4368=ORIENTED_EDGE('',*,*,#3179,.T.);
#4369=ORIENTED_EDGE('',*,*,#3136,.T.);
#4370=ORIENTED_EDGE('',*,*,#3177,.F.);
#4371=ORIENTED_EDGE('',*,*,#3180,.T.);
#4372=ORIENTED_EDGE('',*,*,#3179,.F.);
#4373=ORIENTED_EDGE('',*,*,#3181,.T.);
#4374=ORIENTED_EDGE('',*,*,#3182,.T.);
#4375=ORIENTED_EDGE('',*,*,#3137,.T.);
#4376=ORIENTED_EDGE('',*,*,#3183,.T.);
#4377=ORIENTED_EDGE('',*,*,#3138,.T.);
#4378=ORIENTED_EDGE('',*,*,#3182,.F.);
#4379=ORIENTED_EDGE('',*,*,#3184,.T.);
#4380=ORIENTED_EDGE('',*,*,#3183,.F.);
#4381=ORIENTED_EDGE('',*,*,#3185,.T.);
#4382=ORIENTED_EDGE('',*,*,#3186,.T.);
#4383=ORIENTED_EDGE('',*,*,#3139,.T.);
#4384=ORIENTED_EDGE('',*,*,#3187,.T.);
#4385=ORIENTED_EDGE('',*,*,#3140,.T.);
#4386=ORIENTED_EDGE('',*,*,#3186,.F.);
#4387=ORIENTED_EDGE('',*,*,#3188,.T.);
#4388=ORIENTED_EDGE('',*,*,#3187,.F.);
#4389=ORIENTED_EDGE('',*,*,#3189,.T.);
#4390=ORIENTED_EDGE('',*,*,#3190,.T.);
#4391=ORIENTED_EDGE('',*,*,#3141,.T.);
#4392=ORIENTED_EDGE('',*,*,#3190,.F.);
#4393=ORIENTED_EDGE('',*,*,#3191,.T.);
#4394=ORIENTED_EDGE('',*,*,#3192,.T.);
#4395=ORIENTED_EDGE('',*,*,#3142,.T.);
#4396=ORIENTED_EDGE('',*,*,#3192,.F.);
#4397=ORIENTED_EDGE('',*,*,#3193,.T.);
#4398=ORIENTED_EDGE('',*,*,#3194,.T.);
#4399=ORIENTED_EDGE('',*,*,#3143,.T.);
#4400=ORIENTED_EDGE('',*,*,#3194,.F.);
#4401=ORIENTED_EDGE('',*,*,#3195,.T.);
#4402=ORIENTED_EDGE('',*,*,#3196,.T.);
#4403=ORIENTED_EDGE('',*,*,#3144,.T.);
#4404=ORIENTED_EDGE('',*,*,#3196,.F.);
#4405=ORIENTED_EDGE('',*,*,#3197,.T.);
#4406=ORIENTED_EDGE('',*,*,#3198,.T.);
#4407=ORIENTED_EDGE('',*,*,#3145,.T.);
#4408=ORIENTED_EDGE('',*,*,#3198,.F.);
#4409=ORIENTED_EDGE('',*,*,#3199,.T.);
#4410=ORIENTED_EDGE('',*,*,#3200,.T.);
#4411=ORIENTED_EDGE('',*,*,#3146,.T.);
#4412=ORIENTED_EDGE('',*,*,#3200,.F.);
#4413=ORIENTED_EDGE('',*,*,#3201,.T.);
#4414=ORIENTED_EDGE('',*,*,#3202,.T.);
#4415=ORIENTED_EDGE('',*,*,#3147,.T.);
#4416=ORIENTED_EDGE('',*,*,#3202,.F.);
#4417=ORIENTED_EDGE('',*,*,#3203,.T.);
#4418=ORIENTED_EDGE('',*,*,#3204,.T.);
#4419=ORIENTED_EDGE('',*,*,#3148,.T.);
#4420=ORIENTED_EDGE('',*,*,#3204,.F.);
#4421=ORIENTED_EDGE('',*,*,#3205,.T.);
#4422=ORIENTED_EDGE('',*,*,#3206,.T.);
#4423=ORIENTED_EDGE('',*,*,#3149,.T.);
#4424=ORIENTED_EDGE('',*,*,#3206,.F.);
#4425=ORIENTED_EDGE('',*,*,#3207,.T.);
#4426=ORIENTED_EDGE('',*,*,#3208,.T.);
#4427=ORIENTED_EDGE('',*,*,#3150,.T.);
#4428=ORIENTED_EDGE('',*,*,#3208,.F.);
#4429=ORIENTED_EDGE('',*,*,#3209,.T.);
#4430=ORIENTED_EDGE('',*,*,#3210,.T.);
#4431=ORIENTED_EDGE('',*,*,#3151,.T.);
#4432=ORIENTED_EDGE('',*,*,#3210,.F.);
#4433=ORIENTED_EDGE('',*,*,#3211,.T.);
#4434=ORIENTED_EDGE('',*,*,#3212,.T.);
#4435=ORIENTED_EDGE('',*,*,#3152,.T.);
#4436=ORIENTED_EDGE('',*,*,#3212,.F.);
#4437=ORIENTED_EDGE('',*,*,#3213,.T.);
#4438=ORIENTED_EDGE('',*,*,#3214,.T.);
#4439=ORIENTED_EDGE('',*,*,#3153,.T.);
#4440=ORIENTED_EDGE('',*,*,#3214,.F.);
#4441=ORIENTED_EDGE('',*,*,#3215,.T.);
#4442=ORIENTED_EDGE('',*,*,#3216,.T.);
#4443=ORIENTED_EDGE('',*,*,#3154,.T.);
#4444=ORIENTED_EDGE('',*,*,#3217,.T.);
#4445=ORIENTED_EDGE('',*,*,#3155,.T.);
#4446=ORIENTED_EDGE('',*,*,#3216,.F.);
#4447=ORIENTED_EDGE('',*,*,#3218,.T.);
#4448=ORIENTED_EDGE('',*,*,#3217,.F.);
#4449=ORIENTED_EDGE('',*,*,#3219,.T.);
#4450=ORIENTED_EDGE('',*,*,#3165,.F.);
#4451=ORIENTED_EDGE('',*,*,#3156,.T.);
#4452=ORIENTED_EDGE('',*,*,#3191,.F.);
#4453=ORIENTED_EDGE('',*,*,#3220,.F.);
#4454=ORIENTED_EDGE('',*,*,#3221,.F.);
#4455=ORIENTED_EDGE('',*,*,#3222,.F.);
#4456=ORIENTED_EDGE('',*,*,#3189,.F.);
#4457=ORIENTED_EDGE('',*,*,#3223,.T.);
#4458=ORIENTED_EDGE('',*,*,#3224,.F.);
#4459=ORIENTED_EDGE('',*,*,#3220,.T.);
#4460=ORIENTED_EDGE('',*,*,#3188,.F.);
#4461=ORIENTED_EDGE('',*,*,#3225,.F.);
#4462=ORIENTED_EDGE('',*,*,#3226,.F.);
#4463=ORIENTED_EDGE('',*,*,#3223,.F.);
#4464=ORIENTED_EDGE('',*,*,#3185,.F.);
#4465=ORIENTED_EDGE('',*,*,#3227,.T.);
#4466=ORIENTED_EDGE('',*,*,#3228,.F.);
#4467=ORIENTED_EDGE('',*,*,#3225,.T.);
#4468=ORIENTED_EDGE('',*,*,#3184,.F.);
#4469=ORIENTED_EDGE('',*,*,#3229,.F.);
#4470=ORIENTED_EDGE('',*,*,#3230,.F.);
#4471=ORIENTED_EDGE('',*,*,#3227,.F.);
#4472=ORIENTED_EDGE('',*,*,#3181,.F.);
#4473=ORIENTED_EDGE('',*,*,#3231,.T.);
#4474=ORIENTED_EDGE('',*,*,#3232,.F.);
#4475=ORIENTED_EDGE('',*,*,#3229,.T.);
#4476=ORIENTED_EDGE('',*,*,#3180,.F.);
#4477=ORIENTED_EDGE('',*,*,#3233,.F.);
#4478=ORIENTED_EDGE('',*,*,#3234,.F.);
#4479=ORIENTED_EDGE('',*,*,#3231,.F.);
#4480=ORIENTED_EDGE('',*,*,#3178,.F.);
#4481=ORIENTED_EDGE('',*,*,#3235,.F.);
#4482=ORIENTED_EDGE('',*,*,#3236,.F.);
#4483=ORIENTED_EDGE('',*,*,#3233,.T.);
#4484=ORIENTED_EDGE('',*,*,#3175,.F.);
#4485=ORIENTED_EDGE('',*,*,#3237,.T.);
#4486=ORIENTED_EDGE('',*,*,#3238,.F.);
#4487=ORIENTED_EDGE('',*,*,#3235,.T.);
#4488=ORIENTED_EDGE('',*,*,#3174,.F.);
#4489=ORIENTED_EDGE('',*,*,#3239,.F.);
#4490=ORIENTED_EDGE('',*,*,#3240,.F.);
#4491=ORIENTED_EDGE('',*,*,#3237,.F.);
#4492=ORIENTED_EDGE('',*,*,#3171,.F.);
#4493=ORIENTED_EDGE('',*,*,#3241,.T.);
#4494=ORIENTED_EDGE('',*,*,#3242,.F.);
#4495=ORIENTED_EDGE('',*,*,#3239,.T.);
#4496=ORIENTED_EDGE('',*,*,#3170,.F.);
#4497=ORIENTED_EDGE('',*,*,#3243,.F.);
#4498=ORIENTED_EDGE('',*,*,#3244,.F.);
#4499=ORIENTED_EDGE('',*,*,#3241,.F.);
#4500=ORIENTED_EDGE('',*,*,#3167,.F.);
#4501=ORIENTED_EDGE('',*,*,#3245,.T.);
#4502=ORIENTED_EDGE('',*,*,#3246,.F.);
#4503=ORIENTED_EDGE('',*,*,#3243,.T.);
#4504=ORIENTED_EDGE('',*,*,#3166,.F.);
#4505=ORIENTED_EDGE('',*,*,#3247,.F.);
#4506=ORIENTED_EDGE('',*,*,#3248,.F.);
#4507=ORIENTED_EDGE('',*,*,#3245,.F.);
#4508=ORIENTED_EDGE('',*,*,#3249,.T.);
#4509=ORIENTED_EDGE('',*,*,#3248,.T.);
#4510=ORIENTED_EDGE('',*,*,#3250,.T.);
#4511=ORIENTED_EDGE('',*,*,#3074,.T.);
#4512=ORIENTED_EDGE('',*,*,#3251,.T.);
#4513=ORIENTED_EDGE('',*,*,#3246,.T.);
#4514=ORIENTED_EDGE('',*,*,#3249,.F.);
#4515=ORIENTED_EDGE('',*,*,#3101,.T.);
#4516=ORIENTED_EDGE('',*,*,#3252,.T.);
#4517=ORIENTED_EDGE('',*,*,#3244,.T.);
#4518=ORIENTED_EDGE('',*,*,#3251,.F.);
#4519=ORIENTED_EDGE('',*,*,#3100,.T.);
#4520=ORIENTED_EDGE('',*,*,#3253,.T.);
#4521=ORIENTED_EDGE('',*,*,#3242,.T.);
#4522=ORIENTED_EDGE('',*,*,#3252,.F.);
#4523=ORIENTED_EDGE('',*,*,#3099,.T.);
#4524=ORIENTED_EDGE('',*,*,#3254,.T.);
#4525=ORIENTED_EDGE('',*,*,#3240,.T.);
#4526=ORIENTED_EDGE('',*,*,#3253,.F.);
#4527=ORIENTED_EDGE('',*,*,#3098,.T.);
#4528=ORIENTED_EDGE('',*,*,#3255,.T.);
#4529=ORIENTED_EDGE('',*,*,#3238,.T.);
#4530=ORIENTED_EDGE('',*,*,#3254,.F.);
#4531=ORIENTED_EDGE('',*,*,#3097,.T.);
#4532=ORIENTED_EDGE('',*,*,#3256,.T.);
#4533=ORIENTED_EDGE('',*,*,#3236,.T.);
#4534=ORIENTED_EDGE('',*,*,#3255,.F.);
#4535=ORIENTED_EDGE('',*,*,#3096,.T.);
#4536=ORIENTED_EDGE('',*,*,#3257,.T.);
#4537=ORIENTED_EDGE('',*,*,#3234,.T.);
#4538=ORIENTED_EDGE('',*,*,#3256,.F.);
#4539=ORIENTED_EDGE('',*,*,#3095,.T.);
#4540=ORIENTED_EDGE('',*,*,#3258,.T.);
#4541=ORIENTED_EDGE('',*,*,#3232,.T.);
#4542=ORIENTED_EDGE('',*,*,#3257,.F.);
#4543=ORIENTED_EDGE('',*,*,#3094,.T.);
#4544=ORIENTED_EDGE('',*,*,#3259,.T.);
#4545=ORIENTED_EDGE('',*,*,#3230,.T.);
#4546=ORIENTED_EDGE('',*,*,#3258,.F.);
#4547=ORIENTED_EDGE('',*,*,#3093,.T.);
#4548=ORIENTED_EDGE('',*,*,#3260,.T.);
#4549=ORIENTED_EDGE('',*,*,#3228,.T.);
#4550=ORIENTED_EDGE('',*,*,#3259,.F.);
#4551=ORIENTED_EDGE('',*,*,#3092,.T.);
#4552=ORIENTED_EDGE('',*,*,#3260,.F.);
#4553=ORIENTED_EDGE('',*,*,#3091,.T.);
#4554=ORIENTED_EDGE('',*,*,#3261,.T.);
#4555=ORIENTED_EDGE('',*,*,#3226,.T.);
#4556=ORIENTED_EDGE('',*,*,#3262,.T.);
#4557=ORIENTED_EDGE('',*,*,#3224,.T.);
#4558=ORIENTED_EDGE('',*,*,#3261,.F.);
#4559=ORIENTED_EDGE('',*,*,#3090,.T.);
#4560=ORIENTED_EDGE('',*,*,#3262,.F.);
#4561=ORIENTED_EDGE('',*,*,#3089,.T.);
#4562=ORIENTED_EDGE('',*,*,#3263,.T.);
#4563=ORIENTED_EDGE('',*,*,#3221,.T.);
#4564=ORIENTED_EDGE('',*,*,#3264,.T.);
#4565=ORIENTED_EDGE('',*,*,#3265,.T.);
#4566=ORIENTED_EDGE('',*,*,#3263,.F.);
#4567=ORIENTED_EDGE('',*,*,#3088,.T.);
#4568=ORIENTED_EDGE('',*,*,#3264,.F.);
#4569=ORIENTED_EDGE('',*,*,#3087,.T.);
#4570=ORIENTED_EDGE('',*,*,#3266,.T.);
#4571=ORIENTED_EDGE('',*,*,#3267,.T.);
#4572=ORIENTED_EDGE('',*,*,#3266,.F.);
#4573=ORIENTED_EDGE('',*,*,#3086,.T.);
#4574=ORIENTED_EDGE('',*,*,#3268,.T.);
#4575=ORIENTED_EDGE('',*,*,#3269,.T.);
#4576=ORIENTED_EDGE('',*,*,#3270,.T.);
#4577=ORIENTED_EDGE('',*,*,#3271,.T.);
#4578=ORIENTED_EDGE('',*,*,#3268,.F.);
#4579=ORIENTED_EDGE('',*,*,#3085,.T.);
#4580=ORIENTED_EDGE('',*,*,#3270,.F.);
#4581=ORIENTED_EDGE('',*,*,#3084,.T.);
#4582=ORIENTED_EDGE('',*,*,#3272,.T.);
#4583=ORIENTED_EDGE('',*,*,#3273,.T.);
#4584=ORIENTED_EDGE('',*,*,#3274,.T.);
#4585=ORIENTED_EDGE('',*,*,#3275,.T.);
#4586=ORIENTED_EDGE('',*,*,#3272,.F.);
#4587=ORIENTED_EDGE('',*,*,#3083,.T.);
#4588=ORIENTED_EDGE('',*,*,#3274,.F.);
#4589=ORIENTED_EDGE('',*,*,#3082,.T.);
#4590=ORIENTED_EDGE('',*,*,#3276,.T.);
#4591=ORIENTED_EDGE('',*,*,#3277,.T.);
#4592=ORIENTED_EDGE('',*,*,#3278,.T.);
#4593=ORIENTED_EDGE('',*,*,#3279,.T.);
#4594=ORIENTED_EDGE('',*,*,#3276,.F.);
#4595=ORIENTED_EDGE('',*,*,#3081,.T.);
#4596=ORIENTED_EDGE('',*,*,#3278,.F.);
#4597=ORIENTED_EDGE('',*,*,#3080,.T.);
#4598=ORIENTED_EDGE('',*,*,#3280,.T.);
#4599=ORIENTED_EDGE('',*,*,#3281,.T.);
#4600=ORIENTED_EDGE('',*,*,#3282,.T.);
#4601=ORIENTED_EDGE('',*,*,#3283,.T.);
#4602=ORIENTED_EDGE('',*,*,#3280,.F.);
#4603=ORIENTED_EDGE('',*,*,#3079,.T.);
#4604=ORIENTED_EDGE('',*,*,#3282,.F.);
#4605=ORIENTED_EDGE('',*,*,#3078,.T.);
#4606=ORIENTED_EDGE('',*,*,#3284,.T.);
#4607=ORIENTED_EDGE('',*,*,#3285,.T.);
#4608=ORIENTED_EDGE('',*,*,#3286,.T.);
#4609=ORIENTED_EDGE('',*,*,#3287,.T.);
#4610=ORIENTED_EDGE('',*,*,#3284,.F.);
#4611=ORIENTED_EDGE('',*,*,#3077,.T.);
#4612=ORIENTED_EDGE('',*,*,#3288,.T.);
#4613=ORIENTED_EDGE('',*,*,#3289,.T.);
#4614=ORIENTED_EDGE('',*,*,#3286,.F.);
#4615=ORIENTED_EDGE('',*,*,#3076,.T.);
#4616=ORIENTED_EDGE('',*,*,#3250,.F.);
#4617=ORIENTED_EDGE('',*,*,#3290,.T.);
#4618=ORIENTED_EDGE('',*,*,#3288,.F.);
#4619=ORIENTED_EDGE('',*,*,#3075,.T.);
#4620=ORIENTED_EDGE('',*,*,#3195,.F.);
#4621=ORIENTED_EDGE('',*,*,#3291,.F.);
#4622=ORIENTED_EDGE('',*,*,#3267,.F.);
#4623=ORIENTED_EDGE('',*,*,#3292,.T.);
#4624=ORIENTED_EDGE('',*,*,#3197,.F.);
#4625=ORIENTED_EDGE('',*,*,#3292,.F.);
#4626=ORIENTED_EDGE('',*,*,#3269,.F.);
#4627=ORIENTED_EDGE('',*,*,#3293,.F.);
#4628=ORIENTED_EDGE('',*,*,#3199,.F.);
#4629=ORIENTED_EDGE('',*,*,#3293,.T.);
#4630=ORIENTED_EDGE('',*,*,#3271,.F.);
#4631=ORIENTED_EDGE('',*,*,#3294,.T.);
#4632=ORIENTED_EDGE('',*,*,#3201,.F.);
#4633=ORIENTED_EDGE('',*,*,#3294,.F.);
#4634=ORIENTED_EDGE('',*,*,#3273,.F.);
#4635=ORIENTED_EDGE('',*,*,#3295,.F.);
#4636=ORIENTED_EDGE('',*,*,#3203,.F.);
#4637=ORIENTED_EDGE('',*,*,#3295,.T.);
#4638=ORIENTED_EDGE('',*,*,#3275,.F.);
#4639=ORIENTED_EDGE('',*,*,#3296,.T.);
#4640=ORIENTED_EDGE('',*,*,#3205,.F.);
#4641=ORIENTED_EDGE('',*,*,#3296,.F.);
#4642=ORIENTED_EDGE('',*,*,#3277,.F.);
#4643=ORIENTED_EDGE('',*,*,#3297,.F.);
#4644=ORIENTED_EDGE('',*,*,#3207,.F.);
#4645=ORIENTED_EDGE('',*,*,#3297,.T.);
#4646=ORIENTED_EDGE('',*,*,#3279,.F.);
#4647=ORIENTED_EDGE('',*,*,#3298,.T.);
#4648=ORIENTED_EDGE('',*,*,#3209,.F.);
#4649=ORIENTED_EDGE('',*,*,#3298,.F.);
#4650=ORIENTED_EDGE('',*,*,#3281,.F.);
#4651=ORIENTED_EDGE('',*,*,#3299,.F.);
#4652=ORIENTED_EDGE('',*,*,#3211,.F.);
#4653=ORIENTED_EDGE('',*,*,#3299,.T.);
#4654=ORIENTED_EDGE('',*,*,#3283,.F.);
#4655=ORIENTED_EDGE('',*,*,#3300,.T.);
#4656=ORIENTED_EDGE('',*,*,#3213,.F.);
#4657=ORIENTED_EDGE('',*,*,#3300,.F.);
#4658=ORIENTED_EDGE('',*,*,#3285,.F.);
#4659=ORIENTED_EDGE('',*,*,#3301,.T.);
#4660=ORIENTED_EDGE('',*,*,#3215,.F.);
#4661=ORIENTED_EDGE('',*,*,#3301,.F.);
#4662=ORIENTED_EDGE('',*,*,#3287,.F.);
#4663=ORIENTED_EDGE('',*,*,#3302,.T.);
#4664=ORIENTED_EDGE('',*,*,#3218,.F.);
#4665=ORIENTED_EDGE('',*,*,#3302,.F.);
#4666=ORIENTED_EDGE('',*,*,#3289,.F.);
#4667=ORIENTED_EDGE('',*,*,#3303,.F.);
#4668=ORIENTED_EDGE('',*,*,#3219,.F.);
#4669=ORIENTED_EDGE('',*,*,#3303,.T.);
#4670=ORIENTED_EDGE('',*,*,#3290,.F.);
#4671=ORIENTED_EDGE('',*,*,#3247,.T.);
#4672=ORIENTED_EDGE('',*,*,#3193,.F.);
#4673=ORIENTED_EDGE('',*,*,#3222,.T.);
#4674=ORIENTED_EDGE('',*,*,#3265,.F.);
#4675=ORIENTED_EDGE('',*,*,#3291,.T.);
#4676=ORIENTED_EDGE('',*,*,#3159,.F.);
#4677=ORIENTED_EDGE('',*,*,#3304,.T.);
#4678=ORIENTED_EDGE('',*,*,#3104,.F.);
#4679=ORIENTED_EDGE('',*,*,#3304,.F.);
#4948=PLANE('',#5821);
#4949=PLANE('',#5866);
#4950=PLANE('',#5889);
#4951=PLANE('',#5892);
#4952=PLANE('',#5895);
#4953=PLANE('',#5898);
#4954=PLANE('',#5903);
#4955=PLANE('',#5906);
#4956=PLANE('',#5909);
#4957=PLANE('',#5914);
#4958=PLANE('',#5917);
#4959=PLANE('',#5920);
#4960=PLANE('',#5923);
#4961=PLANE('',#5926);
#4962=PLANE('',#5929);
#4963=PLANE('',#5932);
#4964=PLANE('',#5935);
#4965=PLANE('',#5938);
#4966=PLANE('',#5943);
#4967=PLANE('',#5946);
#4968=PLANE('',#5949);
#4969=PLANE('',#5952);
#4970=PLANE('',#5953);
#4971=PLANE('',#5955);
#4972=PLANE('',#5957);
#4973=PLANE('',#5959);
#4974=PLANE('',#5962);
#4975=PLANE('',#5964);
#4976=PLANE('',#5966);
#4977=PLANE('',#5971);
#4978=PLANE('',#5974);
#4979=PLANE('',#5977);
#4980=PLANE('',#5980);
#4981=PLANE('',#5983);
#4982=PLANE('',#5986);
#4983=PLANE('',#5990);
#4984=PLANE('',#5992);
#4985=PLANE('',#5994);
#4986=PLANE('',#5996);
#4987=PLANE('',#5998);
#4988=PLANE('',#6000);
#5190=ADVANCED_FACE('',(#778),#64,.F.);
#5191=ADVANCED_FACE('',(#779,#153,#154,#155,#156,#157,#158,#159,#160),#4948,
 .F.);
#5192=ADVANCED_FACE('',(#780),#65,.F.);
#5193=ADVANCED_FACE('',(#781),#66,.F.);
#5194=ADVANCED_FACE('',(#782),#227,.F.);
#5195=ADVANCED_FACE('',(#783),#579,.F.);
#5196=ADVANCED_FACE('',(#784),#228,.F.);
#5197=ADVANCED_FACE('',(#785),#580,.F.);
#5198=ADVANCED_FACE('',(#786),#229,.F.);
#5199=ADVANCED_FACE('',(#787),#581,.F.);
#5200=ADVANCED_FACE('',(#788),#230,.F.);
#5201=ADVANCED_FACE('',(#789),#582,.F.);
#5202=ADVANCED_FACE('',(#790),#231,.F.);
#5203=ADVANCED_FACE('',(#791,#161,#162,#163,#164,#165),#4949,.T.);
#5204=ADVANCED_FACE('',(#792),#232,.F.);
#5205=ADVANCED_FACE('',(#793),#233,.F.);
#5206=ADVANCED_FACE('',(#794),#234,.F.);
#5207=ADVANCED_FACE('',(#795),#4950,.T.);
#5208=ADVANCED_FACE('',(#796),#235,.T.);
#5209=ADVANCED_FACE('',(#797),#4951,.T.);
#5210=ADVANCED_FACE('',(#798),#236,.T.);
#5211=ADVANCED_FACE('',(#799),#4952,.T.);
#5212=ADVANCED_FACE('',(#800),#237,.T.);
#5213=ADVANCED_FACE('',(#801),#4953,.T.);
#5214=ADVANCED_FACE('',(#802),#238,.F.);
#5215=ADVANCED_FACE('',(#803),#239,.T.);
#5216=ADVANCED_FACE('',(#804),#4954,.T.);
#5217=ADVANCED_FACE('',(#805),#240,.T.);
#5218=ADVANCED_FACE('',(#806),#4955,.T.);
#5219=ADVANCED_FACE('',(#807),#241,.T.);
#5220=ADVANCED_FACE('',(#808),#4956,.T.);
#5221=ADVANCED_FACE('',(#809),#242,.T.);
#5222=ADVANCED_FACE('',(#810),#243,.F.);
#5223=ADVANCED_FACE('',(#811),#4957,.T.);
#5224=ADVANCED_FACE('',(#812),#244,.T.);
#5225=ADVANCED_FACE('',(#813),#4958,.T.);
#5226=ADVANCED_FACE('',(#814),#245,.T.);
#5227=ADVANCED_FACE('',(#815),#4959,.T.);
#5228=ADVANCED_FACE('',(#816),#246,.T.);
#5229=ADVANCED_FACE('',(#817),#4960,.T.);
#5230=ADVANCED_FACE('',(#818),#247,.T.);
#5231=ADVANCED_FACE('',(#819),#4961,.T.);
#5232=ADVANCED_FACE('',(#820),#248,.T.);
#5233=ADVANCED_FACE('',(#821),#4962,.T.);
#5234=ADVANCED_FACE('',(#822),#249,.T.);
#5235=ADVANCED_FACE('',(#823),#4963,.F.);
#5236=ADVANCED_FACE('',(#824),#583,.T.);
#5237=ADVANCED_FACE('',(#825),#4964,.T.);
#5238=ADVANCED_FACE('',(#826),#584,.T.);
#5239=ADVANCED_FACE('',(#827),#4965,.T.);
#5240=ADVANCED_FACE('',(#828),#585,.T.);
#5241=ADVANCED_FACE('',(#829),#586,.F.);
#5242=ADVANCED_FACE('',(#830),#4966,.T.);
#5243=ADVANCED_FACE('',(#831),#587,.T.);
#5244=ADVANCED_FACE('',(#832),#4967,.T.);
#5245=ADVANCED_FACE('',(#833),#588,.T.);
#5246=ADVANCED_FACE('',(#834),#4968,.T.);
#5247=ADVANCED_FACE('',(#835),#589,.T.);
#5248=ADVANCED_FACE('',(#836),#4969,.T.);
#5249=ADVANCED_FACE('',(#837),#4970,.T.);
#5250=ADVANCED_FACE('',(#838),#250,.T.);
#5251=ADVANCED_FACE('',(#839),#4971,.T.);
#5252=ADVANCED_FACE('',(#840),#251,.T.);
#5253=ADVANCED_FACE('',(#841),#4972,.T.);
#5254=ADVANCED_FACE('',(#842),#252,.T.);
#5255=ADVANCED_FACE('',(#843),#4973,.T.);
#5256=ADVANCED_FACE('',(#844),#253,.F.);
#5257=ADVANCED_FACE('',(#845),#254,.T.);
#5258=ADVANCED_FACE('',(#846),#4974,.T.);
#5259=ADVANCED_FACE('',(#847),#255,.T.);
#5260=ADVANCED_FACE('',(#848),#4975,.T.);
#5261=ADVANCED_FACE('',(#849),#256,.T.);
#5262=ADVANCED_FACE('',(#850),#4976,.T.);
#5263=ADVANCED_FACE('',(#851),#257,.T.);
#5264=ADVANCED_FACE('',(#852),#258,.F.);
#5265=ADVANCED_FACE('',(#853),#4977,.T.);
#5266=ADVANCED_FACE('',(#854),#259,.T.);
#5267=ADVANCED_FACE('',(#855),#4978,.T.);
#5268=ADVANCED_FACE('',(#856),#260,.T.);
#5269=ADVANCED_FACE('',(#857),#4979,.T.);
#5270=ADVANCED_FACE('',(#858),#261,.T.);
#5271=ADVANCED_FACE('',(#859),#4980,.T.);
#5272=ADVANCED_FACE('',(#860),#262,.T.);
#5273=ADVANCED_FACE('',(#861),#4981,.T.);
#5274=ADVANCED_FACE('',(#862),#263,.T.);
#5275=ADVANCED_FACE('',(#863),#4982,.T.);
#5276=ADVANCED_FACE('',(#864),#264,.T.);
#5277=ADVANCED_FACE('',(#865),#590,.F.);
#5278=ADVANCED_FACE('',(#866),#4983,.F.);
#5279=ADVANCED_FACE('',(#867),#591,.T.);
#5280=ADVANCED_FACE('',(#868),#4984,.F.);
#5281=ADVANCED_FACE('',(#869),#592,.T.);
#5282=ADVANCED_FACE('',(#870),#4985,.F.);
#5283=ADVANCED_FACE('',(#871),#593,.T.);
#5284=ADVANCED_FACE('',(#872),#4986,.F.);
#5285=ADVANCED_FACE('',(#873),#594,.T.);
#5286=ADVANCED_FACE('',(#874),#4987,.F.);
#5287=ADVANCED_FACE('',(#875),#595,.T.);
#5288=ADVANCED_FACE('',(#876),#4988,.T.);
#5289=ADVANCED_FACE('',(#877),#596,.T.);
#5290=ADVANCED_FACE('',(#878),#597,.T.);
#5291=ADVANCED_FACE('',(#879),#598,.F.);
#5346=CLOSED_SHELL('',(#5190,#5191,#5192,#5193,#5194,#5195,#5196,#5197,
#5198,#5199,#5200,#5201,#5202,#5203,#5204,#5205,#5206,#5207,#5208,#5209,
#5210,#5211,#5212,#5213,#5214,#5215,#5216,#5217,#5218,#5219,#5220,#5221,
#5222,#5223,#5224,#5225,#5226,#5227,#5228,#5229,#5230,#5231,#5232,#5233,
#5234,#5235,#5236,#5237,#5238,#5239,#5240,#5241,#5242,#5243,#5244,#5245,
#5246,#5247,#5248,#5249,#5250,#5251,#5252,#5253,#5254,#5255,#5256,#5257,
#5258,#5259,#5260,#5261,#5262,#5263,#5264,#5265,#5266,#5267,#5268,#5269,
#5270,#5271,#5272,#5273,#5274,#5275,#5276,#5277,#5278,#5279,#5280,#5281,
#5282,#5283,#5284,#5285,#5286,#5287,#5288,#5289,#5290,#5291));
#5817=AXIS2_PLACEMENT_3D('',#9168,#7010,#7011);
#5818=AXIS2_PLACEMENT_3D('',#9169,#7012,#7013);
#5819=AXIS2_PLACEMENT_3D('',#9171,#7014,#7015);
#5820=AXIS2_PLACEMENT_3D('',#9173,#7016,#7017);
#5821=AXIS2_PLACEMENT_3D('',#9174,#7018,#7019);
#5822=AXIS2_PLACEMENT_3D('',#9179,#7021,#7022);
#5823=AXIS2_PLACEMENT_3D('',#9183,#7024,#7025);
#5824=AXIS2_PLACEMENT_3D('',#9187,#7027,#7028);
#5825=AXIS2_PLACEMENT_3D('',#9191,#7030,#7031);
#5826=AXIS2_PLACEMENT_3D('',#9195,#7033,#7034);
#5827=AXIS2_PLACEMENT_3D('',#9199,#7036,#7037);
#5828=AXIS2_PLACEMENT_3D('',#9203,#7039,#7040);
#5829=AXIS2_PLACEMENT_3D('',#9205,#7041,#7042);
#5830=AXIS2_PLACEMENT_3D('',#9209,#7044,#7045);
#5831=AXIS2_PLACEMENT_3D('',#9213,#7047,#7048);
#5832=AXIS2_PLACEMENT_3D('',#9217,#7050,#7051);
#5833=AXIS2_PLACEMENT_3D('',#9219,#7052,#7053);
#5834=AXIS2_PLACEMENT_3D('',#9223,#7055,#7056);
#5835=AXIS2_PLACEMENT_3D('',#9227,#7058,#7059);
#5836=AXIS2_PLACEMENT_3D('',#9230,#7061,#7062);
#5837=AXIS2_PLACEMENT_3D('',#9232,#7063,#7064);
#5838=AXIS2_PLACEMENT_3D('',#9234,#7065,#7066);
#5839=AXIS2_PLACEMENT_3D('',#9236,#7067,#7068);
#5840=AXIS2_PLACEMENT_3D('',#9238,#7069,#7070);
#5841=AXIS2_PLACEMENT_3D('',#9240,#7071,#7072);
#5842=AXIS2_PLACEMENT_3D('',#9242,#7073,#7074);
#5843=AXIS2_PLACEMENT_3D('',#9244,#7075,#7076);
#5844=AXIS2_PLACEMENT_3D('',#9245,#7077,#7078);
#5845=AXIS2_PLACEMENT_3D('',#9247,#7079,#7080);
#5846=AXIS2_PLACEMENT_3D('',#9248,#7081,#7082);
#5847=AXIS2_PLACEMENT_3D('',#9250,#7083,#7084);
#5848=AXIS2_PLACEMENT_3D('',#9251,#7085,#7086);
#5849=AXIS2_PLACEMENT_3D('',#9254,#7088,#7089);
#5850=AXIS2_PLACEMENT_3D('',#9255,#7090,#7091);
#5851=AXIS2_PLACEMENT_3D('',#9257,#7092,#7093);
#5852=AXIS2_PLACEMENT_3D('',#9259,#7095,#7096);
#5853=AXIS2_PLACEMENT_3D('',#9262,#7098,#7099);
#5854=AXIS2_PLACEMENT_3D('',#9263,#7100,#7101);
#5855=AXIS2_PLACEMENT_3D('',#9265,#7102,#7103);
#5856=AXIS2_PLACEMENT_3D('',#9267,#7105,#7106);
#5857=AXIS2_PLACEMENT_3D('',#9269,#7107,#7108);
#5858=AXIS2_PLACEMENT_3D('',#9271,#7110,#7111);
#5859=AXIS2_PLACEMENT_3D('',#9273,#7112,#7113);
#5860=AXIS2_PLACEMENT_3D('',#9275,#7115,#7116);
#5861=AXIS2_PLACEMENT_3D('',#9277,#7117,#7118);
#5862=AXIS2_PLACEMENT_3D('',#9279,#7120,#7121);
#5863=AXIS2_PLACEMENT_3D('',#9281,#7122,#7123);
#5864=AXIS2_PLACEMENT_3D('',#9283,#7125,#7126);
#5865=AXIS2_PLACEMENT_3D('',#9286,#7128,#7129);
#5866=AXIS2_PLACEMENT_3D('',#9287,#7130,#7131);
#5867=AXIS2_PLACEMENT_3D('',#9292,#7133,#7134);
#5868=AXIS2_PLACEMENT_3D('',#9296,#7136,#7137);
#5869=AXIS2_PLACEMENT_3D('',#9300,#7139,#7140);
#5870=AXIS2_PLACEMENT_3D('',#9304,#7142,#7143);
#5871=AXIS2_PLACEMENT_3D('',#9306,#7144,#7145);
#5872=AXIS2_PLACEMENT_3D('',#9310,#7147,#7148);
#5873=AXIS2_PLACEMENT_3D('',#9314,#7150,#7151);
#5874=AXIS2_PLACEMENT_3D('',#9318,#7153,#7154);
#5875=AXIS2_PLACEMENT_3D('',#9320,#7155,#7156);
#5876=AXIS2_PLACEMENT_3D('',#9324,#7158,#7159);
#5877=AXIS2_PLACEMENT_3D('',#9328,#7161,#7162);
#5878=AXIS2_PLACEMENT_3D('',#9332,#7164,#7165);
#5879=AXIS2_PLACEMENT_3D('',#9336,#7167,#7168);
#5880=AXIS2_PLACEMENT_3D('',#9340,#7170,#7171);
#5881=AXIS2_PLACEMENT_3D('',#9343,#7173,#7174);
#5882=AXIS2_PLACEMENT_3D('',#9345,#7175,#7176);
#5883=AXIS2_PLACEMENT_3D('',#9347,#7177,#7178);
#5884=AXIS2_PLACEMENT_3D('',#9349,#7179,#7180);
#5885=AXIS2_PLACEMENT_3D('',#9351,#7181,#7182);
#5886=AXIS2_PLACEMENT_3D('',#9352,#7183,#7184);
#5887=AXIS2_PLACEMENT_3D('',#9354,#7186,#7187);
#5888=AXIS2_PLACEMENT_3D('',#9356,#7189,#7190);
#5889=AXIS2_PLACEMENT_3D('',#9358,#7192,#7193);
#5890=AXIS2_PLACEMENT_3D('',#9364,#7197,#7198);
#5891=AXIS2_PLACEMENT_3D('',#9366,#7199,#7200);
#5892=AXIS2_PLACEMENT_3D('',#9368,#7202,#7203);
#5893=AXIS2_PLACEMENT_3D('',#9372,#7206,#7207);
#5894=AXIS2_PLACEMENT_3D('',#9374,#7208,#7209);
#5895=AXIS2_PLACEMENT_3D('',#9376,#7211,#7212);
#5896=AXIS2_PLACEMENT_3D('',#9380,#7215,#7216);
#5897=AXIS2_PLACEMENT_3D('',#9382,#7217,#7218);
#5898=AXIS2_PLACEMENT_3D('',#9384,#7220,#7221);
#5899=AXIS2_PLACEMENT_3D('',#9388,#7224,#7225);
#5900=AXIS2_PLACEMENT_3D('',#9391,#7227,#7228);
#5901=AXIS2_PLACEMENT_3D('',#9392,#7229,#7230);
#5902=AXIS2_PLACEMENT_3D('',#9394,#7231,#7232);
#5903=AXIS2_PLACEMENT_3D('',#9396,#7234,#7235);
#5904=AXIS2_PLACEMENT_3D('',#9400,#7238,#7239);
#5905=AXIS2_PLACEMENT_3D('',#9402,#7240,#7241);
#5906=AXIS2_PLACEMENT_3D('',#9404,#7243,#7244);
#5907=AXIS2_PLACEMENT_3D('',#9408,#7247,#7248);
#5908=AXIS2_PLACEMENT_3D('',#9410,#7249,#7250);
#5909=AXIS2_PLACEMENT_3D('',#9412,#7252,#7253);
#5910=AXIS2_PLACEMENT_3D('',#9416,#7256,#7257);
#5911=AXIS2_PLACEMENT_3D('',#9418,#7258,#7259);
#5912=AXIS2_PLACEMENT_3D('',#9420,#7261,#7262);
#5913=AXIS2_PLACEMENT_3D('',#9422,#7263,#7264);
#5914=AXIS2_PLACEMENT_3D('',#9424,#7266,#7267);
#5915=AXIS2_PLACEMENT_3D('',#9428,#7270,#7271);
#5916=AXIS2_PLACEMENT_3D('',#9430,#7272,#7273);
#5917=AXIS2_PLACEMENT_3D('',#9432,#7275,#7276);
#5918=AXIS2_PLACEMENT_3D('',#9436,#7279,#7280);
#5919=AXIS2_PLACEMENT_3D('',#9438,#7281,#7282);
#5920=AXIS2_PLACEMENT_3D('',#9440,#7284,#7285);
#5921=AXIS2_PLACEMENT_3D('',#9444,#7288,#7289);
#5922=AXIS2_PLACEMENT_3D('',#9446,#7290,#7291);
#5923=AXIS2_PLACEMENT_3D('',#9448,#7293,#7294);
#5924=AXIS2_PLACEMENT_3D('',#9452,#7297,#7298);
#5925=AXIS2_PLACEMENT_3D('',#9454,#7299,#7300);
#5926=AXIS2_PLACEMENT_3D('',#9456,#7302,#7303);
#5927=AXIS2_PLACEMENT_3D('',#9460,#7306,#7307);
#5928=AXIS2_PLACEMENT_3D('',#9462,#7308,#7309);
#5929=AXIS2_PLACEMENT_3D('',#9464,#7311,#7312);
#5930=AXIS2_PLACEMENT_3D('',#9468,#7315,#7316);
#5931=AXIS2_PLACEMENT_3D('',#9469,#7317,#7318);
#5932=AXIS2_PLACEMENT_3D('',#9470,#7319,#7320);
#5933=AXIS2_PLACEMENT_3D('',#9476,#7324,#7325);
#5934=AXIS2_PLACEMENT_3D('',#9479,#7327,#7328);
#5935=AXIS2_PLACEMENT_3D('',#9480,#7329,#7330);
#5936=AXIS2_PLACEMENT_3D('',#9484,#7333,#7334);
#5937=AXIS2_PLACEMENT_3D('',#9487,#7336,#7337);
#5938=AXIS2_PLACEMENT_3D('',#9488,#7338,#7339);
#5939=AXIS2_PLACEMENT_3D('',#9492,#7342,#7343);
#5940=AXIS2_PLACEMENT_3D('',#9495,#7345,#7346);
#5941=AXIS2_PLACEMENT_3D('',#9496,#7347,#7348);
#5942=AXIS2_PLACEMENT_3D('',#9499,#7350,#7351);
#5943=AXIS2_PLACEMENT_3D('',#9500,#7352,#7353);
#5944=AXIS2_PLACEMENT_3D('',#9504,#7356,#7357);
#5945=AXIS2_PLACEMENT_3D('',#9507,#7359,#7360);
#5946=AXIS2_PLACEMENT_3D('',#9508,#7361,#7362);
#5947=AXIS2_PLACEMENT_3D('',#9512,#7365,#7366);
#5948=AXIS2_PLACEMENT_3D('',#9515,#7368,#7369);
#5949=AXIS2_PLACEMENT_3D('',#9516,#7370,#7371);
#5950=AXIS2_PLACEMENT_3D('',#9520,#7374,#7375);
#5951=AXIS2_PLACEMENT_3D('',#9523,#7377,#7378);
#5952=AXIS2_PLACEMENT_3D('',#9524,#7379,#7380);
#5953=AXIS2_PLACEMENT_3D('',#9528,#7383,#7384);
#5954=AXIS2_PLACEMENT_3D('',#9531,#7387,#7388);
#5955=AXIS2_PLACEMENT_3D('',#9533,#7390,#7391);
#5956=AXIS2_PLACEMENT_3D('',#9535,#7393,#7394);
#5957=AXIS2_PLACEMENT_3D('',#9537,#7396,#7397);
#5958=AXIS2_PLACEMENT_3D('',#9539,#7399,#7400);
#5959=AXIS2_PLACEMENT_3D('',#9541,#7402,#7403);
#5960=AXIS2_PLACEMENT_3D('',#9543,#7405,#7406);
#5961=AXIS2_PLACEMENT_3D('',#9545,#7408,#7409);
#5962=AXIS2_PLACEMENT_3D('',#9547,#7411,#7412);
#5963=AXIS2_PLACEMENT_3D('',#9549,#7414,#7415);
#5964=AXIS2_PLACEMENT_3D('',#9551,#7417,#7418);
#5965=AXIS2_PLACEMENT_3D('',#9553,#7420,#7421);
#5966=AXIS2_PLACEMENT_3D('',#9555,#7423,#7424);
#5967=AXIS2_PLACEMENT_3D('',#9557,#7426,#7427);
#5968=AXIS2_PLACEMENT_3D('',#9560,#7429,#7430);
#5969=AXIS2_PLACEMENT_3D('',#9561,#7431,#7432);
#5970=AXIS2_PLACEMENT_3D('',#9564,#7434,#7435);
#5971=AXIS2_PLACEMENT_3D('',#9565,#7436,#7437);
#5972=AXIS2_PLACEMENT_3D('',#9569,#7440,#7441);
#5973=AXIS2_PLACEMENT_3D('',#9572,#7443,#7444);
#5974=AXIS2_PLACEMENT_3D('',#9573,#7445,#7446);
#5975=AXIS2_PLACEMENT_3D('',#9577,#7449,#7450);
#5976=AXIS2_PLACEMENT_3D('',#9580,#7452,#7453);
#5977=AXIS2_PLACEMENT_3D('',#9581,#7454,#7455);
#5978=AXIS2_PLACEMENT_3D('',#9585,#7458,#7459);
#5979=AXIS2_PLACEMENT_3D('',#9588,#7461,#7462);
#5980=AXIS2_PLACEMENT_3D('',#9589,#7463,#7464);
#5981=AXIS2_PLACEMENT_3D('',#9593,#7467,#7468);
#5982=AXIS2_PLACEMENT_3D('',#9596,#7470,#7471);
#5983=AXIS2_PLACEMENT_3D('',#9597,#7472,#7473);
#5984=AXIS2_PLACEMENT_3D('',#9601,#7476,#7477);
#5985=AXIS2_PLACEMENT_3D('',#9604,#7479,#7480);
#5986=AXIS2_PLACEMENT_3D('',#9605,#7481,#7482);
#5987=AXIS2_PLACEMENT_3D('',#9609,#7485,#7486);
#5988=AXIS2_PLACEMENT_3D('',#9610,#7487,#7488);
#5989=AXIS2_PLACEMENT_3D('',#9611,#7489,#7490);
#5990=AXIS2_PLACEMENT_3D('',#9614,#7493,#7494);
#5991=AXIS2_PLACEMENT_3D('',#9616,#7496,#7497);
#5992=AXIS2_PLACEMENT_3D('',#9618,#7499,#7500);
#5993=AXIS2_PLACEMENT_3D('',#9620,#7502,#7503);
#5994=AXIS2_PLACEMENT_3D('',#9622,#7505,#7506);
#5995=AXIS2_PLACEMENT_3D('',#9624,#7508,#7509);
#5996=AXIS2_PLACEMENT_3D('',#9626,#7511,#7512);
#5997=AXIS2_PLACEMENT_3D('',#9628,#7514,#7515);
#5998=AXIS2_PLACEMENT_3D('',#9630,#7517,#7518);
#5999=AXIS2_PLACEMENT_3D('',#9632,#7520,#7521);
#6000=AXIS2_PLACEMENT_3D('',#9634,#7523,#7524);
#6001=AXIS2_PLACEMENT_3D('',#9636,#7526,#7527);
#6002=AXIS2_PLACEMENT_3D('',#9637,#7528,#7529);
#6003=AXIS2_PLACEMENT_3D('',#9638,#7530,#7531);
#7010=DIRECTION('axis',(0.,0.,1.));
#7011=DIRECTION('refdir',(1.,0.,0.));
#7012=DIRECTION('center_axis',(0.,0.,-1.));
#7013=DIRECTION('ref_axis',(1.,0.,0.));
#7014=DIRECTION('center_axis',(0.,1.22464679914735E-16,-1.));
#7015=DIRECTION('ref_axis',(0.,1.,1.22464679914735E-16));
#7016=DIRECTION('center_axis',(0.,-1.,-1.22464679914735E-16));
#7017=DIRECTION('ref_axis',(-1.,0.,0.));
#7018=DIRECTION('center_axis',(0.,1.22464679914735E-16,-1.));
#7019=DIRECTION('ref_axis',(1.,0.,0.));
#7020=DIRECTION('',(-0.724137931034482,-0.689655172413793,-8.44583999411968E-17));
#7021=DIRECTION('center_axis',(0.,1.22464679914735E-16,-1.));
#7022=DIRECTION('ref_axis',(0.919145030018057,-0.39391929857917,-4.82412008127351E-17));
#7023=DIRECTION('',(0.,-1.,-1.22464679914735E-16));
#7024=DIRECTION('center_axis',(0.,1.22464679914735E-16,-1.));
#7025=DIRECTION('ref_axis',(0.707106781186548,0.707106781186548,8.65956056235493E-17));
#7026=DIRECTION('',(1.,2.22044604925031E-16,2.71926214689378E-32));
#7027=DIRECTION('center_axis',(0.,1.22464679914735E-16,-1.));
#7028=DIRECTION('ref_axis',(-0.393919298579166,0.919145030018059,1.12562801896381E-16));
#7029=DIRECTION('',(0.689655172413793,0.724137931034483,8.86813199382566E-17));
#7030=DIRECTION('center_axis',(0.,1.22464679914735E-16,-1.));
#7031=DIRECTION('ref_axis',(-0.928476690885259,0.371390676354104,4.54822403030224E-17));
#7032=DIRECTION('',(-2.22044604925031E-16,1.,1.22464679914735E-16));
#7033=DIRECTION('center_axis',(0.,1.22464679914735E-16,-1.));
#7034=DIRECTION('ref_axis',(-0.923879532511288,-0.382683432365088,-4.68652040532628E-17));
#7035=DIRECTION('',(-0.707106781186548,0.707106781186547,8.65956056235493E-17));
#7036=DIRECTION('center_axis',(0.,1.22464679914735E-16,-1.));
#7037=DIRECTION('ref_axis',(-0.382683432365089,-0.923879532511287,-1.1314261122877E-16));
#7038=DIRECTION('',(-1.,-2.22044604925031E-16,-2.71926214689378E-32));
#7039=DIRECTION('center_axis',(0.,-1.22464679914735E-16,1.));
#7040=DIRECTION('ref_axis',(0.363309774563981,-0.931668400079271,-1.14096472402382E-16));
#7041=DIRECTION('center_axis',(0.,1.22464679914735E-16,-1.));
#7042=DIRECTION('ref_axis',(-0.887564039861159,0.460684355220946,5.64175621038594E-17));
#7043=DIRECTION('',(-2.22044604925031E-16,1.,1.22464679914735E-16));
#7044=DIRECTION('center_axis',(0.,1.22464679914735E-16,-1.));
#7045=DIRECTION('ref_axis',(-0.923879532511288,-0.382683432365088,-4.68652040532628E-17));
#7046=DIRECTION('',(-0.707106781186547,0.707106781186548,8.65956056235494E-17));
#7047=DIRECTION('center_axis',(0.,1.22464679914735E-16,-1.));
#7048=DIRECTION('ref_axis',(-0.382683432365094,-0.923879532511285,-1.1314261122877E-16));
#7049=DIRECTION('',(-1.,0.,0.));
#7050=DIRECTION('center_axis',(0.,1.22464679914735E-16,-1.));
#7051=DIRECTION('ref_axis',(0.460684355220946,-0.887564039861159,-1.08695246045426E-16));
#7052=DIRECTION('center_axis',(0.,-1.22464679914735E-16,1.));
#7053=DIRECTION('ref_axis',(-0.931668400079272,0.363309774563981,4.44926152518725E-17));
#7054=DIRECTION('',(0.,1.,1.22464679914735E-16));
#7055=DIRECTION('center_axis',(0.,1.22464679914735E-16,-1.));
#7056=DIRECTION('ref_axis',(-0.923879532511287,-0.382683432365089,-4.68652040532629E-17));
#7057=DIRECTION('',(-0.707106781186547,0.707106781186548,8.65956056235494E-17));
#7058=DIRECTION('center_axis',(0.,1.22464679914735E-16,-1.));
#7059=DIRECTION('ref_axis',(-0.382683432365091,-0.923879532511286,-1.1314261122877E-16));
#7060=DIRECTION('',(-1.,0.,0.));
#7061=DIRECTION('center_axis',(0.,1.22464679914735E-16,-1.));
#7062=DIRECTION('ref_axis',(0.371390676354104,-0.928476690885259,-1.13705600757556E-16));
#7063=DIRECTION('center_axis',(0.,-1.22464679914735E-16,1.));
#7064=DIRECTION('ref_axis',(-2.22044604925031E-16,1.,1.22464679914735E-16));
#7065=DIRECTION('center_axis',(0.,-1.22464679914735E-16,1.));
#7066=DIRECTION('ref_axis',(1.,0.,0.));
#7067=DIRECTION('center_axis',(0.,1.22464679914735E-16,-1.));
#7068=DIRECTION('ref_axis',(-2.22044604925031E-16,1.,1.22464679914735E-16));
#7069=DIRECTION('center_axis',(0.,-1.22464679914735E-16,1.));
#7070=DIRECTION('ref_axis',(1.,0.,0.));
#7071=DIRECTION('center_axis',(0.,-1.22464679914735E-16,1.));
#7072=DIRECTION('ref_axis',(-2.22044604925031E-16,1.,1.22464679914735E-16));
#7073=DIRECTION('center_axis',(0.,1.22464679914735E-16,-1.));
#7074=DIRECTION('ref_axis',(0.,1.,1.22464679914735E-16));
#7075=DIRECTION('center_axis',(0.,1.22464679914735E-16,-1.));
#7076=DIRECTION('ref_axis',(0.,1.,1.22464679914735E-16));
#7077=DIRECTION('center_axis',(0.,0.,-1.));
#7078=DIRECTION('ref_axis',(1.,0.,0.));
#7079=DIRECTION('center_axis',(0.,-1.,-1.22464679914735E-16));
#7080=DIRECTION('ref_axis',(-1.,0.,0.));
#7081=DIRECTION('center_axis',(0.,0.,-1.));
#7082=DIRECTION('ref_axis',(1.,0.,0.));
#7083=DIRECTION('center_axis',(0.,-1.,-1.22464679914735E-16));
#7084=DIRECTION('ref_axis',(-1.,0.,0.));
#7085=DIRECTION('center_axis',(0.,-1.22464679914735E-16,1.));
#7086=DIRECTION('ref_axis',(-2.22044604925031E-16,1.,1.22464679914735E-16));
#7087=DIRECTION('',(-2.43604851491927E-16,0.707106781186547,-0.707106781186548));
#7088=DIRECTION('center_axis',(0.,1.22464679914735E-16,-1.));
#7089=DIRECTION('ref_axis',(-2.22044604925031E-16,1.,1.22464679914735E-16));
#7090=DIRECTION('center_axis',(0.,-1.22464679914735E-16,1.));
#7091=DIRECTION('ref_axis',(-2.22044604925031E-16,1.,1.22464679914735E-16));
#7092=DIRECTION('center_axis',(0.,-1.22464679914735E-16,1.));
#7093=DIRECTION('ref_axis',(-2.22044604925031E-16,1.,1.22464679914735E-16));
#7094=DIRECTION('',(0.,-1.22464679914735E-16,1.));
#7095=DIRECTION('center_axis',(0.,-1.22464679914735E-16,1.));
#7096=DIRECTION('ref_axis',(-2.22044604925031E-16,1.,1.22464679914735E-16));
#7097=DIRECTION('',(-2.43604851491927E-16,0.707106781186547,-0.707106781186548));
#7098=DIRECTION('center_axis',(0.,1.22464679914735E-16,-1.));
#7099=DIRECTION('ref_axis',(-2.22044604925031E-16,1.,1.22464679914735E-16));
#7100=DIRECTION('center_axis',(0.,-1.22464679914735E-16,1.));
#7101=DIRECTION('ref_axis',(-2.22044604925031E-16,1.,1.22464679914735E-16));
#7102=DIRECTION('center_axis',(0.,-1.22464679914735E-16,1.));
#7103=DIRECTION('ref_axis',(-2.22044604925031E-16,1.,1.22464679914735E-16));
#7104=DIRECTION('',(0.,-1.22464679914735E-16,1.));
#7105=DIRECTION('center_axis',(0.,-1.22464679914735E-16,1.));
#7106=DIRECTION('ref_axis',(1.,0.,0.));
#7107=DIRECTION('center_axis',(0.,1.22464679914735E-16,-1.));
#7108=DIRECTION('ref_axis',(1.,0.,0.));
#7109=DIRECTION('',(-0.707106781186547,-9.24446373305873E-32,0.707106781186548));
#7110=DIRECTION('center_axis',(0.,1.22464679914735E-16,-1.));
#7111=DIRECTION('ref_axis',(1.,0.,0.));
#7112=DIRECTION('center_axis',(0.,-1.22464679914735E-16,1.));
#7113=DIRECTION('ref_axis',(1.,0.,0.));
#7114=DIRECTION('',(0.,-1.22464679914735E-16,1.));
#7115=DIRECTION('center_axis',(0.,-1.22464679914735E-16,1.));
#7116=DIRECTION('ref_axis',(1.,0.,0.));
#7117=DIRECTION('center_axis',(0.,1.22464679914735E-16,-1.));
#7118=DIRECTION('ref_axis',(1.,0.,0.));
#7119=DIRECTION('',(-0.707106781186547,-9.24446373305873E-32,0.707106781186548));
#7120=DIRECTION('center_axis',(0.,1.22464679914735E-16,-1.));
#7121=DIRECTION('ref_axis',(1.,0.,0.));
#7122=DIRECTION('center_axis',(0.,-1.22464679914735E-16,1.));
#7123=DIRECTION('ref_axis',(1.,0.,0.));
#7124=DIRECTION('',(0.,-1.22464679914735E-16,1.));
#7125=DIRECTION('center_axis',(0.,1.22464679914735E-16,-1.));
#7126=DIRECTION('ref_axis',(-2.22044604925031E-16,1.,1.22464679914735E-16));
#7127=DIRECTION('',(2.43604851491927E-16,-0.707106781186547,-0.707106781186548));
#7128=DIRECTION('center_axis',(0.,1.22464679914735E-16,-1.));
#7129=DIRECTION('ref_axis',(-2.22044604925031E-16,1.,1.22464679914735E-16));
#7130=DIRECTION('center_axis',(0.,1.22464679914735E-16,-1.));
#7131=DIRECTION('ref_axis',(1.,0.,0.));
#7132=DIRECTION('',(0.724137931034482,0.689655172413793,8.44583999411968E-17));
#7133=DIRECTION('center_axis',(0.,-1.22464679914735E-16,1.));
#7134=DIRECTION('ref_axis',(0.371390676354104,-0.928476690885259,-1.13705600757556E-16));
#7135=DIRECTION('',(1.,0.,0.));
#7136=DIRECTION('center_axis',(0.,-1.22464679914735E-16,1.));
#7137=DIRECTION('ref_axis',(-0.382683432365091,-0.923879532511286,-1.1314261122877E-16));
#7138=DIRECTION('',(0.707106781186547,-0.707106781186548,-8.65956056235494E-17));
#7139=DIRECTION('center_axis',(0.,-1.22464679914735E-16,1.));
#7140=DIRECTION('ref_axis',(-0.923879532511287,-0.382683432365089,-4.68652040532629E-17));
#7141=DIRECTION('',(0.,-1.,-1.22464679914735E-16));
#7142=DIRECTION('center_axis',(0.,1.22464679914735E-16,-1.));
#7143=DIRECTION('ref_axis',(-0.931668400079272,0.363309774563981,4.44926152518725E-17));
#7144=DIRECTION('center_axis',(0.,-1.22464679914735E-16,1.));
#7145=DIRECTION('ref_axis',(0.460684355220946,-0.887564039861159,-1.08695246045426E-16));
#7146=DIRECTION('',(1.,0.,0.));
#7147=DIRECTION('center_axis',(0.,-1.22464679914735E-16,1.));
#7148=DIRECTION('ref_axis',(-0.382683432365094,-0.923879532511285,-1.1314261122877E-16));
#7149=DIRECTION('',(0.707106781186547,-0.707106781186548,-8.65956056235494E-17));
#7150=DIRECTION('center_axis',(0.,-1.22464679914735E-16,1.));
#7151=DIRECTION('ref_axis',(-0.923879532511288,-0.382683432365088,-4.68652040532628E-17));
#7152=DIRECTION('',(2.22044604925031E-16,-1.,-1.22464679914735E-16));
#7153=DIRECTION('center_axis',(0.,-1.22464679914735E-16,1.));
#7154=DIRECTION('ref_axis',(-0.887564039861159,0.460684355220946,5.64175621038594E-17));
#7155=DIRECTION('center_axis',(0.,1.22464679914735E-16,-1.));
#7156=DIRECTION('ref_axis',(0.363309774563981,-0.931668400079271,-1.14096472402382E-16));
#7157=DIRECTION('',(1.,2.22044604925031E-16,2.71926214689378E-32));
#7158=DIRECTION('center_axis',(0.,-1.22464679914735E-16,1.));
#7159=DIRECTION('ref_axis',(-0.382683432365089,-0.923879532511287,-1.1314261122877E-16));
#7160=DIRECTION('',(0.707106781186548,-0.707106781186547,-8.65956056235493E-17));
#7161=DIRECTION('center_axis',(0.,-1.22464679914735E-16,1.));
#7162=DIRECTION('ref_axis',(-0.923879532511287,-0.382683432365088,-4.68652040532628E-17));
#7163=DIRECTION('',(2.22044604925031E-16,-1.,-1.22464679914735E-16));
#7164=DIRECTION('center_axis',(0.,-1.22464679914735E-16,1.));
#7165=DIRECTION('ref_axis',(-0.928476690885259,0.371390676354104,4.54822403030224E-17));
#7166=DIRECTION('',(-0.689655172413793,-0.724137931034483,-8.86813199382566E-17));
#7167=DIRECTION('center_axis',(0.,-1.22464679914735E-16,1.));
#7168=DIRECTION('ref_axis',(-0.393919298579166,0.919145030018059,1.12562801896381E-16));
#7169=DIRECTION('',(-1.,-2.22044604925031E-16,-2.71926214689378E-32));
#7170=DIRECTION('center_axis',(0.,-1.22464679914735E-16,1.));
#7171=DIRECTION('ref_axis',(0.707106781186548,0.707106781186548,8.65956056235493E-17));
#7172=DIRECTION('',(0.,1.,1.22464679914735E-16));
#7173=DIRECTION('center_axis',(0.,-1.22464679914735E-16,1.));
#7174=DIRECTION('ref_axis',(0.919145030018057,-0.39391929857917,-4.82412008127351E-17));
#7175=DIRECTION('center_axis',(0.,1.22464679914735E-16,-1.));
#7176=DIRECTION('ref_axis',(-2.22044604925031E-16,1.,1.22464679914735E-16));
#7177=DIRECTION('center_axis',(0.,1.22464679914735E-16,-1.));
#7178=DIRECTION('ref_axis',(1.,0.,0.));
#7179=DIRECTION('center_axis',(0.,-1.22464679914735E-16,1.));
#7180=DIRECTION('ref_axis',(1.,0.,0.));
#7181=DIRECTION('center_axis',(0.,1.22464679914735E-16,-1.));
#7182=DIRECTION('ref_axis',(1.,0.,0.));
#7183=DIRECTION('center_axis',(0.,1.22464679914735E-16,-1.));
#7184=DIRECTION('ref_axis',(-2.22044604925031E-16,1.,1.22464679914735E-16));
#7185=DIRECTION('',(2.43604851491927E-16,-0.707106781186547,-0.707106781186548));
#7186=DIRECTION('center_axis',(0.,1.22464679914735E-16,-1.));
#7187=DIRECTION('ref_axis',(1.,0.,0.));
#7188=DIRECTION('',(0.707106781186547,-1.73191211247099E-16,0.707106781186548));
#7189=DIRECTION('center_axis',(0.,1.22464679914735E-16,-1.));
#7190=DIRECTION('ref_axis',(1.,0.,0.));
#7191=DIRECTION('',(0.707106781186547,-1.73191211247099E-16,0.707106781186548));
#7192=DIRECTION('center_axis',(0.487659849094173,-0.512042841548881,-0.707106781186545));
#7193=DIRECTION('ref_axis',(0.823212785915304,-6.95272347095421E-17,0.567732955803662));
#7194=DIRECTION('',(-0.48765984909417,0.512042841548878,-0.70710678118655));
#7195=DIRECTION('',(0.48765984909417,-0.512042841548877,0.707106781186549));
#7196=DIRECTION('',(-0.724137931034482,-0.689655172413793,-8.44583999411968E-17));
#7197=DIRECTION('center_axis',(0.,-1.22464679914735E-16,1.));
#7198=DIRECTION('ref_axis',(0.371390676354104,-0.928476690885259,-1.13705600757556E-16));
#7199=DIRECTION('center_axis',(0.,1.22464679914735E-16,-1.));
#7200=DIRECTION('ref_axis',(0.371390676354104,-0.928476690885259,-1.13705600757556E-16));
#7201=DIRECTION('',(0.,0.707106781186549,-0.707106781186546));
#7202=DIRECTION('center_axis',(0.,-0.707106781186549,-0.707106781186546));
#7203=DIRECTION('ref_axis',(1.,0.,0.));
#7204=DIRECTION('',(0.,0.707106781186546,-0.707106781186549));
#7205=DIRECTION('',(-1.,0.,0.));
#7206=DIRECTION('center_axis',(0.,-1.22464679914735E-16,1.));
#7207=DIRECTION('ref_axis',(-0.382683432365091,-0.923879532511286,-1.1314261122877E-16));
#7208=DIRECTION('center_axis',(0.,1.22464679914735E-16,-1.));
#7209=DIRECTION('ref_axis',(-0.382683432365091,-0.923879532511286,-1.1314261122877E-16));
#7210=DIRECTION('',(0.499999999999999,0.499999999999995,-0.707106781186552));
#7211=DIRECTION('center_axis',(-0.500000000000001,-0.5,-0.707106781186547));
#7212=DIRECTION('ref_axis',(0.816496580927725,7.0705015914994E-17,-0.577350269189627));
#7213=DIRECTION('',(0.499999999999998,0.5,-0.707106781186549));
#7214=DIRECTION('',(-0.707106781186547,0.707106781186548,8.65956056235494E-17));
#7215=DIRECTION('center_axis',(0.,-1.22464679914735E-16,1.));
#7216=DIRECTION('ref_axis',(-0.923879532511287,-0.382683432365089,-4.68652040532629E-17));
#7217=DIRECTION('center_axis',(0.,1.22464679914735E-16,-1.));
#7218=DIRECTION('ref_axis',(-0.923879532511287,-0.382683432365089,-4.68652040532629E-17));
#7219=DIRECTION('',(0.707106781186547,8.65956056235493E-17,-0.707106781186547));
#7220=DIRECTION('center_axis',(-0.707106781186548,8.65956056235493E-17,
-0.707106781186548));
#7221=DIRECTION('ref_axis',(0.707106781186548,8.65956056235493E-17,-0.707106781186548));
#7222=DIRECTION('',(0.707106781186547,8.65956056235494E-17,-0.707106781186548));
#7223=DIRECTION('',(0.,1.,1.22464679914735E-16));
#7224=DIRECTION('center_axis',(0.,1.22464679914735E-16,-1.));
#7225=DIRECTION('ref_axis',(-0.931668400079272,0.363309774563981,4.44926152518725E-17));
#7226=DIRECTION('',(-0.578253353382651,0.406968130572547,-0.707106781186551));
#7227=DIRECTION('center_axis',(0.,-1.22464679914735E-16,1.));
#7228=DIRECTION('ref_axis',(-0.931668400079272,0.363309774563981,4.44926152518725E-17));
#7229=DIRECTION('center_axis',(0.,-1.22464679914735E-16,1.));
#7230=DIRECTION('ref_axis',(0.460684355220946,-0.887564039861159,-1.08695246045426E-16));
#7231=DIRECTION('center_axis',(0.,1.22464679914735E-16,-1.));
#7232=DIRECTION('ref_axis',(0.460684355220946,-0.887564039861159,-1.08695246045426E-16));
#7233=DIRECTION('',(0.,0.707106781186549,-0.707106781186546));
#7234=DIRECTION('center_axis',(0.,-0.707106781186549,-0.707106781186546));
#7235=DIRECTION('ref_axis',(1.,0.,0.));
#7236=DIRECTION('',(0.,0.707106781186546,-0.707106781186549));
#7237=DIRECTION('',(-1.,0.,0.));
#7238=DIRECTION('center_axis',(0.,-1.22464679914735E-16,1.));
#7239=DIRECTION('ref_axis',(-0.382683432365094,-0.923879532511285,-1.1314261122877E-16));
#7240=DIRECTION('center_axis',(0.,1.22464679914735E-16,-1.));
#7241=DIRECTION('ref_axis',(-0.382683432365094,-0.923879532511285,-1.1314261122877E-16));
#7242=DIRECTION('',(0.500000000000001,0.499999999999995,-0.707106781186551));
#7243=DIRECTION('center_axis',(-0.500000000000001,-0.5,-0.707106781186547));
#7244=DIRECTION('ref_axis',(0.816496580927725,7.0705015914994E-17,-0.577350269189627));
#7245=DIRECTION('',(0.499999999999999,0.499999999999999,-0.707106781186548));
#7246=DIRECTION('',(-0.707106781186547,0.707106781186548,8.65956056235494E-17));
#7247=DIRECTION('center_axis',(0.,-1.22464679914735E-16,1.));
#7248=DIRECTION('ref_axis',(-0.923879532511287,-0.382683432365088,-4.68652040532628E-17));
#7249=DIRECTION('center_axis',(0.,1.22464679914735E-16,-1.));
#7250=DIRECTION('ref_axis',(-0.923879532511288,-0.382683432365088,-4.68652040532628E-17));
#7251=DIRECTION('',(0.707106781186549,3.22678052299109E-15,-0.707106781186546));
#7252=DIRECTION('center_axis',(-0.707106781186549,-7.04136402448287E-17,
-0.707106781186546));
#7253=DIRECTION('ref_axis',(0.707106781186546,8.65956056235495E-17,-0.707106781186549));
#7254=DIRECTION('',(-2.22044604925031E-16,1.,1.22464679914735E-16));
#7255=DIRECTION('',(0.707106781186546,8.65956056235495E-17,-0.707106781186549));
#7256=DIRECTION('center_axis',(0.,-1.22464679914735E-16,1.));
#7257=DIRECTION('ref_axis',(-0.887564039861159,0.460684355220946,5.64175621038594E-17));
#7258=DIRECTION('center_axis',(0.,1.22464679914735E-16,-1.));
#7259=DIRECTION('ref_axis',(-0.887564039861159,0.460684355220946,5.64175621038594E-17));
#7260=DIRECTION('',(0.406968130572545,-0.578253353382658,-0.707106781186547));
#7261=DIRECTION('center_axis',(0.,1.22464679914735E-16,-1.));
#7262=DIRECTION('ref_axis',(0.363309774563981,-0.931668400079272,-1.14096472402382E-16));
#7263=DIRECTION('center_axis',(0.,-1.22464679914735E-16,1.));
#7264=DIRECTION('ref_axis',(0.363309774563981,-0.931668400079271,-1.14096472402382E-16));
#7265=DIRECTION('',(0.,0.707106781186546,-0.707106781186549));
#7266=DIRECTION('center_axis',(1.57009245868378E-16,-0.707106781186547,
-0.707106781186548));
#7267=DIRECTION('ref_axis',(1.,-2.71926214689378E-32,2.22044604925031E-16));
#7268=DIRECTION('',(-1.,-2.22044604925031E-16,-2.71926214689378E-32));
#7269=DIRECTION('',(0.,0.707106781186548,-0.707106781186547));
#7270=DIRECTION('center_axis',(0.,-1.22464679914735E-16,1.));
#7271=DIRECTION('ref_axis',(-0.382683432365089,-0.923879532511287,-1.1314261122877E-16));
#7272=DIRECTION('center_axis',(0.,1.22464679914735E-16,-1.));
#7273=DIRECTION('ref_axis',(-0.382683432365089,-0.923879532511287,-1.1314261122877E-16));
#7274=DIRECTION('',(0.499999999999999,0.500000000000001,-0.707106781186548));
#7275=DIRECTION('center_axis',(-0.500000000000001,-0.500000000000002,-0.707106781186545));
#7276=DIRECTION('ref_axis',(0.816496580927724,7.07050159149941E-17,-0.577350269189628));
#7277=DIRECTION('',(-0.707106781186548,0.707106781186547,8.65956056235493E-17));
#7278=DIRECTION('',(0.499999999999997,0.500000000000001,-0.707106781186549));
#7279=DIRECTION('center_axis',(0.,-1.22464679914735E-16,1.));
#7280=DIRECTION('ref_axis',(-0.923879532511287,-0.382683432365088,-4.68652040532628E-17));
#7281=DIRECTION('center_axis',(0.,1.22464679914735E-16,-1.));
#7282=DIRECTION('ref_axis',(-0.923879532511287,-0.382683432365088,-4.68652040532628E-17));
#7283=DIRECTION('',(0.707106781186546,8.65956056235495E-17,-0.707106781186549));
#7284=DIRECTION('center_axis',(-0.707106781186549,-7.04136402448287E-17,
-0.707106781186546));
#7285=DIRECTION('ref_axis',(0.707106781186546,8.65956056235495E-17,-0.707106781186549));
#7286=DIRECTION('',(-2.22044604925031E-16,1.,1.22464679914735E-16));
#7287=DIRECTION('',(0.707106781186546,8.65956056235495E-17,-0.707106781186549));
#7288=DIRECTION('center_axis',(0.,-1.22464679914735E-16,1.));
#7289=DIRECTION('ref_axis',(-0.928476690885259,0.371390676354104,4.54822403030224E-17));
#7290=DIRECTION('center_axis',(0.,1.22464679914735E-16,-1.));
#7291=DIRECTION('ref_axis',(-0.928476690885259,0.371390676354104,4.54822403030224E-17));
#7292=DIRECTION('',(0.512042841548877,-0.487659849094171,-0.707106781186549));
#7293=DIRECTION('center_axis',(-0.512042841548879,0.487659849094171,-0.707106781186547));
#7294=DIRECTION('ref_axis',(0.809942121543021,7.1826736412027E-17,-0.586509812151843));
#7295=DIRECTION('',(0.689655172413793,0.724137931034483,8.86813199382566E-17));
#7296=DIRECTION('',(0.512042841548878,-0.487659849094171,-0.707106781186548));
#7297=DIRECTION('center_axis',(0.,-1.22464679914735E-16,1.));
#7298=DIRECTION('ref_axis',(-0.393919298579166,0.919145030018059,1.12562801896381E-16));
#7299=DIRECTION('center_axis',(0.,1.22464679914735E-16,-1.));
#7300=DIRECTION('ref_axis',(-0.393919298579166,0.919145030018059,1.12562801896381E-16));
#7301=DIRECTION('',(0.,-0.707106781186547,-0.707106781186548));
#7302=DIRECTION('center_axis',(-1.57009245868377E-16,0.707106781186547,
-0.707106781186548));
#7303=DIRECTION('ref_axis',(1.,2.71926214689378E-32,-2.22044604925031E-16));
#7304=DIRECTION('',(1.,2.22044604925031E-16,2.71926214689378E-32));
#7305=DIRECTION('',(0.,-0.707106781186549,-0.707106781186546));
#7306=DIRECTION('center_axis',(0.,-1.22464679914735E-16,1.));
#7307=DIRECTION('ref_axis',(0.707106781186547,0.707106781186547,8.65956056235493E-17));
#7308=DIRECTION('center_axis',(0.,1.22464679914735E-16,-1.));
#7309=DIRECTION('ref_axis',(0.707106781186548,0.707106781186547,8.65956056235493E-17));
#7310=DIRECTION('',(-0.707106781186547,-6.98450623718338E-16,-0.707106781186548));
#7311=DIRECTION('center_axis',(0.707106781186548,8.65956056235493E-17,-0.707106781186547));
#7312=DIRECTION('ref_axis',(0.707106781186547,-8.65956056235494E-17,0.707106781186548));
#7313=DIRECTION('',(-0.707106781186547,8.65956056235494E-17,-0.707106781186548));
#7314=DIRECTION('',(0.,-1.,-1.22464679914735E-16));
#7315=DIRECTION('center_axis',(0.,-1.22464679914735E-16,1.));
#7316=DIRECTION('ref_axis',(0.919145030018057,-0.39391929857917,-4.82412008127351E-17));
#7317=DIRECTION('center_axis',(0.,1.22464679914735E-16,-1.));
#7318=DIRECTION('ref_axis',(0.919145030018057,-0.39391929857917,-4.82412008127351E-17));
#7319=DIRECTION('center_axis',(1.,2.22044604925031E-16,2.71926214689378E-32));
#7320=DIRECTION('ref_axis',(2.22044604925031E-16,-1.,-1.22464679914735E-16));
#7321=DIRECTION('',(0.,1.22464679914735E-16,-1.));
#7322=DIRECTION('',(2.22044604925031E-16,-1.,-1.22464679914735E-16));
#7323=DIRECTION('',(0.,-1.22464679914735E-16,1.));
#7324=DIRECTION('center_axis',(0.,1.22464679914735E-16,-1.));
#7325=DIRECTION('ref_axis',(-0.923879532511288,-0.382683432365088,-4.68652040532628E-17));
#7326=DIRECTION('',(0.,-1.22464679914735E-16,1.));
#7327=DIRECTION('center_axis',(0.,-1.22464679914735E-16,1.));
#7328=DIRECTION('ref_axis',(-0.923879532511288,-0.382683432365088,-4.68652040532628E-17));
#7329=DIRECTION('center_axis',(-0.707106781186548,-0.707106781186547,-8.65956056235492E-17));
#7330=DIRECTION('ref_axis',(-0.707106781186547,0.707106781186548,8.65956056235494E-17));
#7331=DIRECTION('',(0.,1.22464679914735E-16,-1.));
#7332=DIRECTION('',(0.707106781186547,-0.707106781186548,-8.65956056235494E-17));
#7333=DIRECTION('center_axis',(0.,1.22464679914735E-16,-1.));
#7334=DIRECTION('ref_axis',(-0.382683432365094,-0.923879532511285,-1.1314261122877E-16));
#7335=DIRECTION('',(0.,-1.22464679914735E-16,1.));
#7336=DIRECTION('center_axis',(0.,-1.22464679914735E-16,1.));
#7337=DIRECTION('ref_axis',(-0.382683432365094,-0.923879532511285,-1.1314261122877E-16));
#7338=DIRECTION('center_axis',(0.,-1.,-1.22464679914735E-16));
#7339=DIRECTION('ref_axis',(-1.,0.,0.));
#7340=DIRECTION('',(0.,1.22464679914735E-16,-1.));
#7341=DIRECTION('',(1.,0.,0.));
#7342=DIRECTION('center_axis',(0.,1.22464679914735E-16,-1.));
#7343=DIRECTION('ref_axis',(0.460684355220946,-0.887564039861159,-1.08695246045426E-16));
#7344=DIRECTION('',(0.,-1.22464679914735E-16,1.));
#7345=DIRECTION('center_axis',(0.,-1.22464679914735E-16,1.));
#7346=DIRECTION('ref_axis',(0.460684355220946,-0.887564039861159,-1.08695246045426E-16));
#7347=DIRECTION('center_axis',(0.,1.22464679914735E-16,-1.));
#7348=DIRECTION('ref_axis',(-0.931668400079272,0.363309774563981,4.44926152518725E-17));
#7349=DIRECTION('',(0.,1.22464679914735E-16,-1.));
#7350=DIRECTION('center_axis',(0.,1.22464679914735E-16,-1.));
#7351=DIRECTION('ref_axis',(-0.931668400079272,0.363309774563981,4.44926152518725E-17));
#7352=DIRECTION('center_axis',(-1.,0.,0.));
#7353=DIRECTION('ref_axis',(0.,1.,1.22464679914735E-16));
#7354=DIRECTION('',(0.,1.22464679914735E-16,-1.));
#7355=DIRECTION('',(0.,-1.,-1.22464679914735E-16));
#7356=DIRECTION('center_axis',(0.,1.22464679914735E-16,-1.));
#7357=DIRECTION('ref_axis',(-0.923879532511287,-0.382683432365089,-4.68652040532629E-17));
#7358=DIRECTION('',(0.,-1.22464679914735E-16,1.));
#7359=DIRECTION('center_axis',(0.,-1.22464679914735E-16,1.));
#7360=DIRECTION('ref_axis',(-0.923879532511287,-0.382683432365089,-4.68652040532629E-17));
#7361=DIRECTION('center_axis',(-0.707106781186548,-0.707106781186547,-8.65956056235493E-17));
#7362=DIRECTION('ref_axis',(-0.707106781186547,0.707106781186548,8.65956056235494E-17));
#7363=DIRECTION('',(0.,1.22464679914735E-16,-1.));
#7364=DIRECTION('',(0.707106781186547,-0.707106781186548,-8.65956056235494E-17));
#7365=DIRECTION('center_axis',(0.,1.22464679914735E-16,-1.));
#7366=DIRECTION('ref_axis',(-0.382683432365091,-0.923879532511286,-1.1314261122877E-16));
#7367=DIRECTION('',(0.,-1.22464679914735E-16,1.));
#7368=DIRECTION('center_axis',(0.,-1.22464679914735E-16,1.));
#7369=DIRECTION('ref_axis',(-0.382683432365091,-0.923879532511286,-1.1314261122877E-16));
#7370=DIRECTION('center_axis',(0.,-1.,-1.22464679914735E-16));
#7371=DIRECTION('ref_axis',(-1.,0.,0.));
#7372=DIRECTION('',(0.,1.22464679914735E-16,-1.));
#7373=DIRECTION('',(1.,0.,0.));
#7374=DIRECTION('center_axis',(0.,1.22464679914735E-16,-1.));
#7375=DIRECTION('ref_axis',(0.371390676354104,-0.928476690885259,-1.13705600757556E-16));
#7376=DIRECTION('',(0.,-1.22464679914735E-16,1.));
#7377=DIRECTION('center_axis',(0.,-1.22464679914735E-16,1.));
#7378=DIRECTION('ref_axis',(0.371390676354104,-0.928476690885259,-1.13705600757556E-16));
#7379=DIRECTION('center_axis',(0.689655172413793,-0.724137931034482,-8.86813199382566E-17));
#7380=DIRECTION('ref_axis',(-0.724137931034482,-0.689655172413793,-8.44583999411968E-17));
#7381=DIRECTION('',(0.,1.22464679914735E-16,-1.));
#7382=DIRECTION('',(0.724137931034482,0.689655172413793,8.44583999411968E-17));
#7383=DIRECTION('center_axis',(0.487659849094172,-0.512042841548881,0.707106781186545));
#7384=DIRECTION('ref_axis',(-0.823212785915305,-6.9527234709542E-17,0.567732955803662));
#7385=DIRECTION('',(0.487659849094171,-0.512042841548877,-0.707106781186549));
#7386=DIRECTION('',(-0.487659849094171,0.512042841548877,0.707106781186549));
#7387=DIRECTION('center_axis',(0.,1.22464679914735E-16,-1.));
#7388=DIRECTION('ref_axis',(0.371390676354104,-0.928476690885259,-1.13705600757556E-16));
#7389=DIRECTION('',(0.,-0.707106781186549,-0.707106781186546));
#7390=DIRECTION('center_axis',(0.,-0.707106781186549,0.707106781186546));
#7391=DIRECTION('ref_axis',(-1.,0.,0.));
#7392=DIRECTION('',(0.,-0.707106781186546,-0.707106781186549));
#7393=DIRECTION('center_axis',(0.,1.22464679914735E-16,-1.));
#7394=DIRECTION('ref_axis',(-0.382683432365091,-0.923879532511286,-1.1314261122877E-16));
#7395=DIRECTION('',(-0.499999999999999,-0.499999999999995,-0.707106781186552));
#7396=DIRECTION('center_axis',(-0.5,-0.5,0.707106781186548));
#7397=DIRECTION('ref_axis',(-0.816496580927726,7.07050159149938E-17,-0.577350269189626));
#7398=DIRECTION('',(-0.5,-0.499999999999999,-0.707106781186548));
#7399=DIRECTION('center_axis',(0.,1.22464679914735E-16,-1.));
#7400=DIRECTION('ref_axis',(-0.923879532511287,-0.382683432365089,-4.68652040532629E-17));
#7401=DIRECTION('',(-0.707106781186547,8.65956056235493E-17,-0.707106781186547));
#7402=DIRECTION('center_axis',(-0.707106781186548,-8.65956056235493E-17,
0.707106781186548));
#7403=DIRECTION('ref_axis',(-0.707106781186548,8.65956056235493E-17,-0.707106781186548));
#7404=DIRECTION('',(-0.707106781186547,8.65956056235494E-17,-0.707106781186548));
#7405=DIRECTION('center_axis',(0.,-1.22464679914735E-16,1.));
#7406=DIRECTION('ref_axis',(-0.931668400079272,0.363309774563981,4.44926152518725E-17));
#7407=DIRECTION('',(0.578253353382651,-0.406968130572547,-0.707106781186551));
#7408=DIRECTION('center_axis',(0.,1.22464679914735E-16,-1.));
#7409=DIRECTION('ref_axis',(0.460684355220946,-0.887564039861159,-1.08695246045426E-16));
#7410=DIRECTION('',(0.,-0.707106781186549,-0.707106781186546));
#7411=DIRECTION('center_axis',(0.,-0.707106781186549,0.707106781186546));
#7412=DIRECTION('ref_axis',(-1.,0.,0.));
#7413=DIRECTION('',(0.,-0.707106781186546,-0.707106781186549));
#7414=DIRECTION('center_axis',(0.,1.22464679914735E-16,-1.));
#7415=DIRECTION('ref_axis',(-0.382683432365094,-0.923879532511285,-1.1314261122877E-16));
#7416=DIRECTION('',(-0.500000000000001,-0.499999999999994,-0.707106781186551));
#7417=DIRECTION('center_axis',(-0.500000000000001,-0.5,0.707106781186546));
#7418=DIRECTION('ref_axis',(-0.816496580927725,7.0705015914994E-17,-0.577350269189627));
#7419=DIRECTION('',(-0.499999999999999,-0.499999999999999,-0.707106781186549));
#7420=DIRECTION('center_axis',(0.,1.22464679914735E-16,-1.));
#7421=DIRECTION('ref_axis',(-0.923879532511287,-0.382683432365088,-4.68652040532628E-17));
#7422=DIRECTION('',(-0.707106781186549,-3.05358931174399E-15,-0.707106781186546));
#7423=DIRECTION('center_axis',(-0.707106781186549,-2.43604851491927E-16,
0.707106781186546));
#7424=DIRECTION('ref_axis',(-0.707106781186546,8.65956056235495E-17,-0.707106781186549));
#7425=DIRECTION('',(-0.707106781186546,8.65956056235495E-17,-0.707106781186549));
#7426=DIRECTION('center_axis',(0.,1.22464679914735E-16,-1.));
#7427=DIRECTION('ref_axis',(-0.887564039861159,0.460684355220946,5.64175621038594E-17));
#7428=DIRECTION('',(-0.406968130572545,0.578253353382658,-0.707106781186547));
#7429=DIRECTION('center_axis',(0.,-1.22464679914735E-16,1.));
#7430=DIRECTION('ref_axis',(-0.887564039861159,0.460684355220946,5.64175621038594E-17));
#7431=DIRECTION('center_axis',(0.,-1.22464679914735E-16,1.));
#7432=DIRECTION('ref_axis',(0.363309774563981,-0.931668400079272,-1.14096472402382E-16));
#7433=DIRECTION('',(0.,-0.707106781186546,-0.707106781186549));
#7434=DIRECTION('center_axis',(0.,1.22464679914735E-16,-1.));
#7435=DIRECTION('ref_axis',(0.363309774563981,-0.931668400079271,-1.14096472402382E-16));
#7436=DIRECTION('center_axis',(1.57009245868378E-16,-0.707106781186548,
0.707106781186547));
#7437=DIRECTION('ref_axis',(-1.,-2.71926214689378E-32,2.22044604925031E-16));
#7438=DIRECTION('',(0.,-0.707106781186547,-0.707106781186548));
#7439=DIRECTION('',(1.,2.22044604925031E-16,2.71926214689378E-32));
#7440=DIRECTION('center_axis',(0.,1.22464679914735E-16,-1.));
#7441=DIRECTION('ref_axis',(-0.382683432365089,-0.923879532511287,-1.1314261122877E-16));
#7442=DIRECTION('',(-0.499999999999999,-0.499999999999999,-0.707106781186549));
#7443=DIRECTION('center_axis',(0.,-1.22464679914735E-16,1.));
#7444=DIRECTION('ref_axis',(-0.382683432365089,-0.923879532511287,-1.1314261122877E-16));
#7445=DIRECTION('center_axis',(-0.499999999999997,-0.499999999999998,0.707106781186551));
#7446=DIRECTION('ref_axis',(-0.816496580927729,7.07050159149933E-17,-0.577350269189622));
#7447=DIRECTION('',(-0.500000000000002,-0.500000000000005,-0.707106781186543));
#7448=DIRECTION('',(0.707106781186548,-0.707106781186547,-8.65956056235493E-17));
#7449=DIRECTION('center_axis',(0.,1.22464679914735E-16,-1.));
#7450=DIRECTION('ref_axis',(-0.923879532511287,-0.382683432365088,-4.68652040532628E-17));
#7451=DIRECTION('',(-0.707106781186546,8.65956056235495E-17,-0.707106781186549));
#7452=DIRECTION('center_axis',(0.,-1.22464679914735E-16,1.));
#7453=DIRECTION('ref_axis',(-0.923879532511287,-0.382683432365088,-4.68652040532628E-17));
#7454=DIRECTION('center_axis',(-0.707106781186549,-2.43604851491927E-16,
0.707106781186546));
#7455=DIRECTION('ref_axis',(-0.707106781186546,8.65956056235495E-17,-0.707106781186549));
#7456=DIRECTION('',(-0.707106781186546,8.65956056235495E-17,-0.707106781186549));
#7457=DIRECTION('',(2.22044604925031E-16,-1.,-1.22464679914735E-16));
#7458=DIRECTION('center_axis',(0.,1.22464679914735E-16,-1.));
#7459=DIRECTION('ref_axis',(-0.928476690885259,0.371390676354104,4.54822403030224E-17));
#7460=DIRECTION('',(-0.512042841548877,0.487659849094171,-0.707106781186549));
#7461=DIRECTION('center_axis',(0.,-1.22464679914735E-16,1.));
#7462=DIRECTION('ref_axis',(-0.928476690885259,0.371390676354104,4.54822403030224E-17));
#7463=DIRECTION('center_axis',(-0.51204284154888,0.487659849094172,0.707106781186546));
#7464=DIRECTION('ref_axis',(-0.80994212154302,7.18267364120272E-17,-0.586509812151845));
#7465=DIRECTION('',(-0.512042841548877,0.48765984909417,-0.707106781186549));
#7466=DIRECTION('',(-0.689655172413793,-0.724137931034483,-8.86813199382566E-17));
#7467=DIRECTION('center_axis',(0.,1.22464679914735E-16,-1.));
#7468=DIRECTION('ref_axis',(-0.393919298579166,0.919145030018059,1.12562801896381E-16));
#7469=DIRECTION('',(0.,0.707106781186548,-0.707106781186547));
#7470=DIRECTION('center_axis',(0.,-1.22464679914735E-16,1.));
#7471=DIRECTION('ref_axis',(-0.393919298579166,0.919145030018059,1.12562801896381E-16));
#7472=DIRECTION('center_axis',(-1.57009245868377E-16,0.707106781186547,
0.707106781186548));
#7473=DIRECTION('ref_axis',(-1.,2.71926214689378E-32,-2.22044604925031E-16));
#7474=DIRECTION('',(0.,0.707106781186549,-0.707106781186546));
#7475=DIRECTION('',(-1.,-2.22044604925031E-16,-2.71926214689378E-32));
#7476=DIRECTION('center_axis',(0.,1.22464679914735E-16,-1.));
#7477=DIRECTION('ref_axis',(0.707106781186547,0.707106781186547,8.65956056235493E-17));
#7478=DIRECTION('',(0.707106781186547,8.71641834965437E-16,-0.707106781186548));
#7479=DIRECTION('center_axis',(0.,-1.22464679914735E-16,1.));
#7480=DIRECTION('ref_axis',(0.707106781186548,0.707106781186547,8.65956056235493E-17));
#7481=DIRECTION('center_axis',(0.707106781186548,-8.65956056235493E-17,
0.707106781186547));
#7482=DIRECTION('ref_axis',(-0.707106781186547,-8.65956056235494E-17,0.707106781186548));
#7483=DIRECTION('',(0.707106781186547,8.65956056235494E-17,-0.707106781186548));
#7484=DIRECTION('',(0.,1.,1.22464679914735E-16));
#7485=DIRECTION('center_axis',(0.,1.22464679914735E-16,-1.));
#7486=DIRECTION('ref_axis',(0.919145030018057,-0.39391929857917,-4.82412008127351E-17));
#7487=DIRECTION('center_axis',(0.,-1.22464679914735E-16,1.));
#7488=DIRECTION('ref_axis',(0.919145030018057,-0.39391929857917,-4.82412008127351E-17));
#7489=DIRECTION('center_axis',(0.,-1.22464679914735E-16,1.));
#7490=DIRECTION('ref_axis',(0.363309774563981,-0.931668400079271,-1.14096472402382E-16));
#7491=DIRECTION('',(0.,1.22464679914735E-16,-1.));
#7492=DIRECTION('',(0.,1.22464679914735E-16,-1.));
#7493=DIRECTION('center_axis',(-2.22044604925031E-16,1.,1.22464679914735E-16));
#7494=DIRECTION('ref_axis',(1.,2.22044604925031E-16,2.71926214689378E-32));
#7495=DIRECTION('',(0.,-1.22464679914735E-16,1.));
#7496=DIRECTION('center_axis',(0.,1.22464679914735E-16,-1.));
#7497=DIRECTION('ref_axis',(-0.382683432365089,-0.923879532511287,-1.1314261122877E-16));
#7498=DIRECTION('',(0.,1.22464679914735E-16,-1.));
#7499=DIRECTION('center_axis',(0.707106781186547,0.707106781186548,8.65956056235494E-17));
#7500=DIRECTION('ref_axis',(0.707106781186548,-0.707106781186547,-8.65956056235493E-17));
#7501=DIRECTION('',(0.,-1.22464679914735E-16,1.));
#7502=DIRECTION('center_axis',(0.,1.22464679914735E-16,-1.));
#7503=DIRECTION('ref_axis',(-0.923879532511287,-0.382683432365088,-4.68652040532628E-17));
#7504=DIRECTION('',(0.,1.22464679914735E-16,-1.));
#7505=DIRECTION('center_axis',(1.,2.22044604925031E-16,2.71926214689378E-32));
#7506=DIRECTION('ref_axis',(2.22044604925031E-16,-1.,-1.22464679914735E-16));
#7507=DIRECTION('',(0.,-1.22464679914735E-16,1.));
#7508=DIRECTION('center_axis',(0.,1.22464679914735E-16,-1.));
#7509=DIRECTION('ref_axis',(-0.928476690885259,0.371390676354104,4.54822403030224E-17));
#7510=DIRECTION('',(0.,1.22464679914735E-16,-1.));
#7511=DIRECTION('center_axis',(0.724137931034483,-0.689655172413793,-8.44583999411968E-17));
#7512=DIRECTION('ref_axis',(-0.689655172413793,-0.724137931034483,-8.86813199382566E-17));
#7513=DIRECTION('',(0.,-1.22464679914735E-16,1.));
#7514=DIRECTION('center_axis',(0.,1.22464679914735E-16,-1.));
#7515=DIRECTION('ref_axis',(-0.393919298579166,0.919145030018059,1.12562801896381E-16));
#7516=DIRECTION('',(0.,1.22464679914735E-16,-1.));
#7517=DIRECTION('center_axis',(2.22044604925031E-16,-1.,-1.22464679914735E-16));
#7518=DIRECTION('ref_axis',(-1.,-2.22044604925031E-16,-2.71926214689378E-32));
#7519=DIRECTION('',(0.,1.22464679914735E-16,-1.));
#7520=DIRECTION('center_axis',(0.,1.22464679914735E-16,-1.));
#7521=DIRECTION('ref_axis',(0.707106781186547,0.707106781186548,8.65956056235493E-17));
#7522=DIRECTION('',(0.,1.22464679914735E-16,-1.));
#7523=DIRECTION('center_axis',(1.,0.,0.));
#7524=DIRECTION('ref_axis',(0.,-1.,-1.22464679914735E-16));
#7525=DIRECTION('',(0.,-1.22464679914735E-16,1.));
#7526=DIRECTION('center_axis',(0.,1.22464679914735E-16,-1.));
#7527=DIRECTION('ref_axis',(0.919145030018057,-0.39391929857917,-4.82412008127351E-17));
#7528=DIRECTION('center_axis',(0.,1.22464679914735E-16,-1.));
#7529=DIRECTION('ref_axis',(-0.887564039861159,0.460684355220946,5.64175621038594E-17));
#7530=DIRECTION('center_axis',(0.,1.22464679914735E-16,-1.));
#7531=DIRECTION('ref_axis',(1.,0.,0.));
#7532=DIRECTION('',(0.,-1.22464679914735E-16,1.));
#9168=CARTESIAN_POINT('',(0.,0.,0.));
#9169=CARTESIAN_POINT('Origin',(-4.88927830720691,5.31072169279307,9.2));
#9170=CARTESIAN_POINT('',(-7.48735451856022,5.31072169279307,7.7));
#9171=CARTESIAN_POINT('Origin',(-4.88927830720691,5.31072169279307,7.7));
#9172=CARTESIAN_POINT('',(-4.88927830720691,5.31072169279307,6.2));
#9173=CARTESIAN_POINT('Origin',(-4.88927830720691,5.31072169279307,9.2));
#9174=CARTESIAN_POINT('Origin',(-11.4815115348679,14.3472131187871,7.7));
#9175=CARTESIAN_POINT('',(-1.50492583139032,3.29514581742751,7.7));
#9176=CARTESIAN_POINT('',(-3.54346119653592,1.3536835649079,7.69999999999999));
#9177=CARTESIAN_POINT('',(-1.20576175806249,3.58006398250164,7.7));
#9178=CARTESIAN_POINT('',(-1.34975341759722,3.65721478294476,7.7));
#9179=CARTESIAN_POINT('Origin',(-1.84975341759722,3.65721478294476,7.7));
#9180=CARTESIAN_POINT('',(-1.34975341759722,25.1502465824028,7.7));
#9181=CARTESIAN_POINT('',(-1.34975341759722,19.7487298505949,7.7));
#9182=CARTESIAN_POINT('',(-4.84975341759722,28.6502465824028,7.7));
#9183=CARTESIAN_POINT('Origin',(-4.84975341759722,25.1502465824028,7.7));
#9184=CARTESIAN_POINT('',(-26.3427852170552,28.6502465824028,7.7));
#9185=CARTESIAN_POINT('',(-8.16563247623254,28.6502465824028,7.7));
#9186=CARTESIAN_POINT('',(-26.7048541825725,28.4950741686097,7.7));
#9187=CARTESIAN_POINT('Origin',(-26.3427852170552,28.1502465824028,7.7));
#9188=CARTESIAN_POINT('',(-28.6463164350921,26.4565388034641,7.7));
#9189=CARTESIAN_POINT('',(-26.4695350109151,28.74215929885,7.7));
#9190=CARTESIAN_POINT('',(-28.7842474695749,26.1117112172572,7.7));
#9191=CARTESIAN_POINT('Origin',(-28.2842474695748,26.1117112172572,7.7));
#9192=CARTESIAN_POINT('',(-28.7842474695749,24.1035614526515,7.7));
#9193=CARTESIAN_POINT('',(-28.7842474695749,20.4294621680221,7.7));
#9194=CARTESIAN_POINT('',(-28.6378008601681,23.7500080620583,7.7));
#9195=CARTESIAN_POINT('Origin',(-28.2842474695748,24.1035614526515,7.7));
#9196=CARTESIAN_POINT('',(-26.5545620724644,21.6667692743546,7.7));
#9197=CARTESIAN_POINT('',(-22.144476402432,17.2566836043221,7.7));
#9198=CARTESIAN_POINT('',(-26.2010086818712,21.5203226649479,7.7));
#9199=CARTESIAN_POINT('Origin',(-26.2010086818712,22.0203226649479,7.7));
#9200=CARTESIAN_POINT('',(-24.6787384375659,21.5203226649479,7.7));
#9201=CARTESIAN_POINT('',(-19.0483668895561,21.5203226649479,7.7));
#9202=CARTESIAN_POINT('',(-23.2398888132926,16.9758883278442,7.7));
#9203=CARTESIAN_POINT('Origin',(-24.6787384375659,19.0203226649479,7.7));
#9204=CARTESIAN_POINT('',(-23.452118888438,16.5670014604234,7.7));
#9205=CARTESIAN_POINT('Origin',(-22.952118888438,16.5670014604234,7.7));
#9206=CARTESIAN_POINT('',(-23.452118888438,10.1397931465341,7.7));
#9207=CARTESIAN_POINT('',(-23.452118888438,15.7520994917882,7.7));
#9208=CARTESIAN_POINT('',(-23.3056722790312,9.78623975594079,7.7));
#9209=CARTESIAN_POINT('Origin',(-22.952118888438,10.1397931465341,7.7));
#9210=CARTESIAN_POINT('',(-20.2137602440592,6.69432772096875,7.7));
#9211=CARTESIAN_POINT('',(-19.7974728068092,6.27804028371878,7.7));
#9212=CARTESIAN_POINT('',(-19.8602068534659,6.54788111156203,7.7));
#9213=CARTESIAN_POINT('Origin',(-19.8602068534659,7.04788111156203,7.7));
#9214=CARTESIAN_POINT('',(-13.4329985395765,6.54788111156204,7.7));
#9215=CARTESIAN_POINT('',(-12.1622628350393,6.54788111156203,7.7));
#9216=CARTESIAN_POINT('',(-13.0241116721558,6.76011118670738,7.7));
#9217=CARTESIAN_POINT('Origin',(-13.4329985395765,7.04788111156204,7.7));
#9218=CARTESIAN_POINT('',(-8.47967733505213,5.32126156243407,7.7));
#9219=CARTESIAN_POINT('Origin',(-10.9796773350521,5.32126156243407,7.7));
#9220=CARTESIAN_POINT('',(-8.47967733505213,3.79899131812881,7.7));
#9221=CARTESIAN_POINT('',(-8.47967733505213,8.86599543727138,7.7));
#9222=CARTESIAN_POINT('',(-8.3332307256454,3.44543792753554,7.7));
#9223=CARTESIAN_POINT('Origin',(-7.97967733505213,3.79899131812881,7.7));
#9224=CARTESIAN_POINT('',(-6.24999193794173,1.36219913983186,7.69999999999999));
#9225=CARTESIAN_POINT('',(-10.6576787225053,5.76988592439547,7.7));
#9226=CARTESIAN_POINT('',(-5.89643854734845,1.21575253042514,7.69999999999999));
#9227=CARTESIAN_POINT('Origin',(-5.89643854734845,1.71575253042514,7.69999999999999));
#9228=CARTESIAN_POINT('',(-3.88828878274281,1.21575253042514,7.69999999999999));
#9229=CARTESIAN_POINT('',(-7.48490015880533,1.21575253042514,7.69999999999999));
#9230=CARTESIAN_POINT('Origin',(-3.88828878274281,1.71575253042514,7.69999999999999));
#9231=CARTESIAN_POINT('',(-10.8648573190427,23.3513464861378,7.7));
#9232=CARTESIAN_POINT('Origin',(-10.8648573190427,25.1013464861378,7.7));
#9233=CARTESIAN_POINT('',(-6.64865351386214,11.2651426809573,7.7));
#9234=CARTESIAN_POINT('Origin',(-4.89865351386214,11.2651426809573,7.7));
#9235=CARTESIAN_POINT('',(-20.801482994706,15.198517005294,7.7));
#9236=CARTESIAN_POINT('Origin',(-14.801482994706,15.198517005294,7.7));
#9237=CARTESIAN_POINT('',(-6.64865351386214,19.1351426809573,7.7));
#9238=CARTESIAN_POINT('Origin',(-4.89865351386214,19.1351426809573,7.7));
#9239=CARTESIAN_POINT('',(-18.7348573190427,23.3513464861378,7.7));
#9240=CARTESIAN_POINT('Origin',(-18.7348573190427,25.1013464861378,7.7));
#9241=CARTESIAN_POINT('',(-27.2873545185602,25.1107216927931,7.7));
#9242=CARTESIAN_POINT('Origin',(-24.6892783072069,25.1107216927931,7.7));
#9243=CARTESIAN_POINT('',(-7.48735451856023,25.1107216927931,7.7));
#9244=CARTESIAN_POINT('Origin',(-4.88927830720691,25.1107216927931,7.7));
#9245=CARTESIAN_POINT('Origin',(-4.88927830720691,25.1107216927931,9.2));
#9246=CARTESIAN_POINT('',(-4.88927830720691,25.1107216927931,6.2));
#9247=CARTESIAN_POINT('Origin',(-4.88927830720691,25.1107216927931,9.2));
#9248=CARTESIAN_POINT('Origin',(-24.6892783072069,25.1107216927931,9.2));
#9249=CARTESIAN_POINT('',(-24.6892783072069,25.1107216927931,6.2));
#9250=CARTESIAN_POINT('Origin',(-24.6892783072069,25.1107216927931,9.2));
#9251=CARTESIAN_POINT('Origin',(-18.7348573190427,25.1013464861378,7.45));
#9252=CARTESIAN_POINT('',(-18.7348573190427,23.8513464861378,7.2));
#9253=CARTESIAN_POINT('',(-18.7348573190427,23.6013464861378,7.45));
#9254=CARTESIAN_POINT('Origin',(-18.7348573190427,25.1013464861378,7.2));
#9255=CARTESIAN_POINT('Origin',(-18.7348573190427,25.1013464861378,19.));
#9256=CARTESIAN_POINT('',(-18.7348573190427,23.8513464861378,1.1));
#9257=CARTESIAN_POINT('Origin',(-18.7348573190427,25.1013464861378,1.1));
#9258=CARTESIAN_POINT('',(-18.7348573190427,23.8513464861378,19.));
#9259=CARTESIAN_POINT('Origin',(-10.8648573190427,25.1013464861379,7.45));
#9260=CARTESIAN_POINT('',(-10.8648573190427,23.8513464861378,7.2));
#9261=CARTESIAN_POINT('',(-10.8648573190427,23.6013464861379,7.45));
#9262=CARTESIAN_POINT('Origin',(-10.8648573190427,25.1013464861379,7.2));
#9263=CARTESIAN_POINT('Origin',(-10.8648573190427,25.1013464861378,19.));
#9264=CARTESIAN_POINT('',(-10.8648573190427,23.8513464861379,1.1));
#9265=CARTESIAN_POINT('Origin',(-10.8648573190427,25.1013464861379,1.1));
#9266=CARTESIAN_POINT('',(-10.8648573190427,23.8513464861378,19.));
#9267=CARTESIAN_POINT('Origin',(-4.89865351386214,19.1351426809573,7.45));
#9268=CARTESIAN_POINT('',(-6.14865351386214,19.1351426809573,7.2));
#9269=CARTESIAN_POINT('Origin',(-4.89865351386214,19.1351426809573,7.2));
#9270=CARTESIAN_POINT('',(-6.39865351386215,19.1351426809573,7.45));
#9271=CARTESIAN_POINT('Origin',(-4.89865351386214,19.1351426809573,19.));
#9272=CARTESIAN_POINT('',(-6.14865351386214,19.1351426809573,1.1));
#9273=CARTESIAN_POINT('Origin',(-4.89865351386214,19.1351426809573,1.1));
#9274=CARTESIAN_POINT('',(-6.14865351386214,19.1351426809573,19.));
#9275=CARTESIAN_POINT('Origin',(-4.89865351386214,11.2651426809573,7.45));
#9276=CARTESIAN_POINT('',(-6.14865351386214,11.2651426809573,7.2));
#9277=CARTESIAN_POINT('Origin',(-4.89865351386214,11.2651426809573,7.2));
#9278=CARTESIAN_POINT('',(-6.39865351386215,11.2651426809573,7.45));
#9279=CARTESIAN_POINT('Origin',(-4.89865351386214,11.2651426809573,19.));
#9280=CARTESIAN_POINT('',(-6.14865351386214,11.2651426809573,1.1));
#9281=CARTESIAN_POINT('Origin',(-4.89865351386214,11.2651426809573,1.1));
#9282=CARTESIAN_POINT('',(-6.14865351386214,11.2651426809573,19.));
#9283=CARTESIAN_POINT('Origin',(-18.7348573190427,25.1013464861378,0.850000000000002));
#9284=CARTESIAN_POINT('',(-18.7348573190427,23.3513464861378,0.600000000000003));
#9285=CARTESIAN_POINT('',(-18.7348573190427,23.6013464861378,0.850000000000002));
#9286=CARTESIAN_POINT('Origin',(-18.7348573190427,25.1013464861378,0.600000000000003));
#9287=CARTESIAN_POINT('Origin',(-11.4815115348679,14.3472131187871,0.600000000000001));
#9288=CARTESIAN_POINT('',(-3.54346119653592,1.35368356490791,0.599999999999998));
#9289=CARTESIAN_POINT('',(-1.50492583139032,3.29514581742752,0.600000000000001));
#9290=CARTESIAN_POINT('',(-1.20576175806249,3.58006398250165,0.600000000000001));
#9291=CARTESIAN_POINT('',(-3.88828878274281,1.21575253042515,0.599999999999998));
#9292=CARTESIAN_POINT('Origin',(-3.88828878274281,1.71575253042515,0.599999999999998));
#9293=CARTESIAN_POINT('',(-5.89643854734845,1.21575253042515,0.599999999999998));
#9294=CARTESIAN_POINT('',(-7.48490015880533,1.21575253042515,0.599999999999998));
#9295=CARTESIAN_POINT('',(-6.24999193794173,1.36219913983187,0.599999999999998));
#9296=CARTESIAN_POINT('Origin',(-5.89643854734845,1.71575253042515,0.599999999999998));
#9297=CARTESIAN_POINT('',(-8.3332307256454,3.44543792753555,0.600000000000001));
#9298=CARTESIAN_POINT('',(-10.6576787225053,5.76988592439548,0.600000000000001));
#9299=CARTESIAN_POINT('',(-8.47967733505213,3.79899131812882,0.600000000000001));
#9300=CARTESIAN_POINT('Origin',(-7.97967733505213,3.79899131812882,0.600000000000001));
#9301=CARTESIAN_POINT('',(-8.47967733505213,5.32126156243408,0.600000000000001));
#9302=CARTESIAN_POINT('',(-8.47967733505213,8.86599543727139,0.600000000000001));
#9303=CARTESIAN_POINT('',(-13.0241116721558,6.76011118670738,0.600000000000001));
#9304=CARTESIAN_POINT('Origin',(-10.9796773350521,5.32126156243408,0.600000000000001));
#9305=CARTESIAN_POINT('',(-13.4329985395765,6.54788111156205,0.600000000000001));
#9306=CARTESIAN_POINT('Origin',(-13.4329985395765,7.04788111156204,0.600000000000001));
#9307=CARTESIAN_POINT('',(-19.8602068534659,6.54788111156204,0.600000000000001));
#9308=CARTESIAN_POINT('',(-12.1622628350393,6.54788111156204,0.600000000000001));
#9309=CARTESIAN_POINT('',(-20.2137602440592,6.69432772096876,0.600000000000001));
#9310=CARTESIAN_POINT('Origin',(-19.8602068534659,7.04788111156204,0.600000000000001));
#9311=CARTESIAN_POINT('',(-23.3056722790312,9.7862397559408,0.600000000000001));
#9312=CARTESIAN_POINT('',(-19.7974728068092,6.27804028371878,0.600000000000001));
#9313=CARTESIAN_POINT('',(-23.452118888438,10.1397931465341,0.600000000000001));
#9314=CARTESIAN_POINT('Origin',(-22.952118888438,10.1397931465341,0.600000000000001));
#9315=CARTESIAN_POINT('',(-23.452118888438,16.5670014604234,0.600000000000001));
#9316=CARTESIAN_POINT('',(-23.452118888438,15.7520994917882,0.600000000000001));
#9317=CARTESIAN_POINT('',(-23.2398888132926,16.9758883278442,0.600000000000001));
#9318=CARTESIAN_POINT('Origin',(-22.952118888438,16.5670014604234,0.600000000000001));
#9319=CARTESIAN_POINT('',(-24.6787384375659,21.5203226649479,0.600000000000003));
#9320=CARTESIAN_POINT('Origin',(-24.6787384375659,19.0203226649479,0.600000000000001));
#9321=CARTESIAN_POINT('',(-26.2010086818712,21.5203226649479,0.600000000000003));
#9322=CARTESIAN_POINT('',(-19.0483668895561,21.5203226649479,0.600000000000003));
#9323=CARTESIAN_POINT('',(-26.5545620724644,21.6667692743546,0.600000000000003));
#9324=CARTESIAN_POINT('Origin',(-26.2010086818712,22.0203226649479,0.600000000000003));
#9325=CARTESIAN_POINT('',(-28.6378008601681,23.7500080620583,0.600000000000003));
#9326=CARTESIAN_POINT('',(-22.144476402432,17.2566836043221,0.600000000000001));
#9327=CARTESIAN_POINT('',(-28.7842474695749,24.1035614526515,0.600000000000003));
#9328=CARTESIAN_POINT('Origin',(-28.2842474695748,24.1035614526515,0.600000000000003));
#9329=CARTESIAN_POINT('',(-28.7842474695749,26.1117112172572,0.600000000000003));
#9330=CARTESIAN_POINT('',(-28.7842474695749,20.4294621680221,0.600000000000001));
#9331=CARTESIAN_POINT('',(-28.6463164350921,26.4565388034641,0.600000000000003));
#9332=CARTESIAN_POINT('Origin',(-28.2842474695748,26.1117112172572,0.600000000000003));
#9333=CARTESIAN_POINT('',(-26.7048541825725,28.4950741686097,0.600000000000003));
#9334=CARTESIAN_POINT('',(-26.4695350109151,28.74215929885,0.600000000000003));
#9335=CARTESIAN_POINT('',(-26.3427852170552,28.6502465824028,0.600000000000003));
#9336=CARTESIAN_POINT('Origin',(-26.3427852170552,28.1502465824028,0.600000000000003));
#9337=CARTESIAN_POINT('',(-4.84975341759722,28.6502465824028,0.600000000000003));
#9338=CARTESIAN_POINT('',(-8.16563247623254,28.6502465824028,0.600000000000003));
#9339=CARTESIAN_POINT('',(-1.34975341759722,25.1502465824028,0.600000000000003));
#9340=CARTESIAN_POINT('Origin',(-4.84975341759722,25.1502465824028,0.600000000000003));
#9341=CARTESIAN_POINT('',(-1.34975341759722,3.65721478294477,0.600000000000001));
#9342=CARTESIAN_POINT('',(-1.34975341759722,19.7487298505949,0.600000000000001));
#9343=CARTESIAN_POINT('Origin',(-1.84975341759722,3.65721478294477,0.600000000000001));
#9344=CARTESIAN_POINT('',(-10.8648573190427,23.3513464861378,0.600000000000003));
#9345=CARTESIAN_POINT('Origin',(-10.8648573190427,25.1013464861379,0.600000000000003));
#9346=CARTESIAN_POINT('',(-6.64865351386214,11.2651426809573,0.600000000000001));
#9347=CARTESIAN_POINT('Origin',(-4.89865351386214,11.2651426809573,0.600000000000001));
#9348=CARTESIAN_POINT('',(-20.801482994706,15.198517005294,0.600000000000001));
#9349=CARTESIAN_POINT('Origin',(-14.801482994706,15.198517005294,0.600000000000001));
#9350=CARTESIAN_POINT('',(-6.64865351386214,19.1351426809573,0.600000000000001));
#9351=CARTESIAN_POINT('Origin',(-4.89865351386214,19.1351426809573,0.600000000000001));
#9352=CARTESIAN_POINT('Origin',(-10.8648573190427,25.1013464861379,0.850000000000002));
#9353=CARTESIAN_POINT('',(-10.8648573190427,23.6013464861379,0.850000000000002));
#9354=CARTESIAN_POINT('Origin',(-4.89865351386214,19.1351426809573,0.85));
#9355=CARTESIAN_POINT('',(-6.39865351386215,19.1351426809573,0.85));
#9356=CARTESIAN_POINT('Origin',(-4.89865351386214,11.2651426809573,0.85));
#9357=CARTESIAN_POINT('',(-6.39865351386215,11.2651426809573,0.85));
#9358=CARTESIAN_POINT('Origin',(-1.03334796495904,3.39902949974303,0.85));
#9359=CARTESIAN_POINT('',(-3.19863361032902,0.99161459939066,1.1));
#9360=CARTESIAN_POINT('',(-3.19863361032902,0.99161459939066,1.1));
#9361=CARTESIAN_POINT('',(-1.16009824518343,2.93307685191027,1.1));
#9362=CARTESIAN_POINT('',(-1.50492583139032,3.29514581742752,0.600000000000001));
#9363=CARTESIAN_POINT('',(-0.860934171855591,3.21799501698441,1.1));
#9364=CARTESIAN_POINT('Origin',(-3.88828878274281,1.71575253042515,0.849999999999997));
#9365=CARTESIAN_POINT('',(-3.88828878274281,0.715752530425142,1.1));
#9366=CARTESIAN_POINT('Origin',(-3.88828878274281,1.71575253042514,1.1));
#9367=CARTESIAN_POINT('',(-3.88828878274281,0.715752530425142,1.1));
#9368=CARTESIAN_POINT('Origin',(-7.48490015880533,0.96575253042515,0.849999999999997));
#9369=CARTESIAN_POINT('',(-5.89643854734845,0.715752530425142,1.1));
#9370=CARTESIAN_POINT('',(-5.89643854734845,0.715752530425142,1.1));
#9371=CARTESIAN_POINT('',(-7.48490015880533,0.715752530425142,1.1));
#9372=CARTESIAN_POINT('Origin',(-5.89643854734845,1.71575253042515,0.849999999999997));
#9373=CARTESIAN_POINT('',(-6.603545328535,1.00864574923859,1.1));
#9374=CARTESIAN_POINT('Origin',(-5.89643854734845,1.71575253042514,1.1));
#9375=CARTESIAN_POINT('',(-6.603545328535,1.00864574923859,1.1));
#9376=CARTESIAN_POINT('Origin',(-10.834455417802,5.59310922909884,0.85));
#9377=CARTESIAN_POINT('',(-8.68678411623867,3.09188453694227,1.1));
#9378=CARTESIAN_POINT('',(-8.68678411623867,3.09188453694227,1.1));
#9379=CARTESIAN_POINT('',(-11.0112321130986,5.4163325338022,1.1));
#9380=CARTESIAN_POINT('Origin',(-7.97967733505213,3.79899131812882,0.85));
#9381=CARTESIAN_POINT('',(-8.97967733505213,3.79899131812881,1.1));
#9382=CARTESIAN_POINT('Origin',(-7.97967733505213,3.79899131812881,1.1));
#9383=CARTESIAN_POINT('',(-8.97967733505213,3.79899131812881,1.1));
#9384=CARTESIAN_POINT('Origin',(-8.72967733505213,8.86599543727139,0.85));
#9385=CARTESIAN_POINT('',(-8.97967733505212,5.32126156243407,1.1));
#9386=CARTESIAN_POINT('',(-8.97967733505212,5.32126156243407,1.1));
#9387=CARTESIAN_POINT('',(-8.97967733505213,8.86599543727138,1.1));
#9388=CARTESIAN_POINT('Origin',(-10.9796773350521,5.32126156243408,0.85));
#9389=CARTESIAN_POINT('',(-12.6152248047351,6.47234126185272,1.1));
#9390=CARTESIAN_POINT('',(-12.6152248047351,6.47234126185272,1.1));
#9391=CARTESIAN_POINT('Origin',(-10.9796773350521,5.32126156243407,1.1));
#9392=CARTESIAN_POINT('Origin',(-13.4329985395765,7.04788111156204,0.85));
#9393=CARTESIAN_POINT('',(-13.4329985395765,6.04788111156203,1.1));
#9394=CARTESIAN_POINT('Origin',(-13.4329985395765,7.04788111156204,1.1));
#9395=CARTESIAN_POINT('',(-13.4329985395765,6.04788111156203,1.1));
#9396=CARTESIAN_POINT('Origin',(-12.1622628350393,6.29788111156204,0.85));
#9397=CARTESIAN_POINT('',(-19.8602068534659,6.04788111156203,1.1));
#9398=CARTESIAN_POINT('',(-19.8602068534659,6.04788111156203,1.1));
#9399=CARTESIAN_POINT('',(-12.1622628350393,6.04788111156203,1.1));
#9400=CARTESIAN_POINT('Origin',(-19.8602068534659,7.04788111156204,0.85));
#9401=CARTESIAN_POINT('',(-20.5673136346525,6.34077433037548,1.1));
#9402=CARTESIAN_POINT('Origin',(-19.8602068534659,7.04788111156203,1.1));
#9403=CARTESIAN_POINT('',(-20.5673136346525,6.34077433037548,1.1));
#9404=CARTESIAN_POINT('Origin',(-19.9742495021059,6.10126358842215,0.85));
#9405=CARTESIAN_POINT('',(-23.6592256696245,9.43268636534752,1.1));
#9406=CARTESIAN_POINT('',(-23.6592256696245,9.43268636534752,1.1));
#9407=CARTESIAN_POINT('',(-20.1510261974025,5.9244868931255,1.1));
#9408=CARTESIAN_POINT('Origin',(-22.952118888438,10.1397931465341,0.85));
#9409=CARTESIAN_POINT('',(-23.952118888438,10.1397931465341,1.1));
#9410=CARTESIAN_POINT('Origin',(-22.952118888438,10.1397931465341,1.1));
#9411=CARTESIAN_POINT('',(-23.952118888438,10.1397931465341,1.1));
#9412=CARTESIAN_POINT('Origin',(-23.702118888438,15.7520994917882,0.85));
#9413=CARTESIAN_POINT('',(-23.952118888438,16.5670014604234,1.1));
#9414=CARTESIAN_POINT('',(-23.952118888438,15.7520994917882,1.1));
#9415=CARTESIAN_POINT('',(-23.952118888438,16.5670014604234,1.1));
#9416=CARTESIAN_POINT('Origin',(-22.952118888438,16.5670014604234,0.85));
#9417=CARTESIAN_POINT('',(-23.5276587381473,17.3847751952649,1.1));
#9418=CARTESIAN_POINT('Origin',(-22.952118888438,16.5670014604234,1.1));
#9419=CARTESIAN_POINT('',(-23.5276587381473,17.3847751952649,1.1));
#9420=CARTESIAN_POINT('Origin',(-24.6787384375659,19.0203226649479,0.85));
#9421=CARTESIAN_POINT('',(-24.6787384375659,21.0203226649479,1.10000000000001));
#9422=CARTESIAN_POINT('Origin',(-24.6787384375659,19.0203226649479,1.1));
#9423=CARTESIAN_POINT('',(-24.6787384375659,21.0203226649479,1.10000000000001));
#9424=CARTESIAN_POINT('Origin',(-19.0483668895561,21.2703226649479,0.850000000000002));
#9425=CARTESIAN_POINT('',(-26.2010086818712,21.0203226649479,1.10000000000001));
#9426=CARTESIAN_POINT('',(-19.0483668895561,21.0203226649479,1.10000000000001));
#9427=CARTESIAN_POINT('',(-26.2010086818712,21.0203226649479,1.10000000000001));
#9428=CARTESIAN_POINT('Origin',(-26.2010086818712,22.0203226649479,0.850000000000002));
#9429=CARTESIAN_POINT('',(-26.9081154630577,21.3132158837613,1.10000000000001));
#9430=CARTESIAN_POINT('Origin',(-26.2010086818712,22.0203226649479,1.1));
#9431=CARTESIAN_POINT('',(-26.9081154630577,21.3132158837613,1.10000000000001));
#9432=CARTESIAN_POINT('Origin',(-22.3212530977286,17.0799069090255,0.850000000000002));
#9433=CARTESIAN_POINT('',(-28.9913542507614,23.396454671465,1.10000000000001));
#9434=CARTESIAN_POINT('',(-22.4980297930252,16.9031302137289,1.1));
#9435=CARTESIAN_POINT('',(-28.9913542507614,23.396454671465,1.10000000000001));
#9436=CARTESIAN_POINT('Origin',(-28.2842474695748,24.1035614526515,0.850000000000002));
#9437=CARTESIAN_POINT('',(-29.2842474695749,24.1035614526515,1.1));
#9438=CARTESIAN_POINT('Origin',(-28.2842474695748,24.1035614526515,1.1));
#9439=CARTESIAN_POINT('',(-29.2842474695749,24.1035614526515,1.1));
#9440=CARTESIAN_POINT('Origin',(-29.0342474695749,20.4294621680221,0.85));
#9441=CARTESIAN_POINT('',(-29.2842474695749,26.1117112172572,1.1));
#9442=CARTESIAN_POINT('',(-29.2842474695749,20.4294621680221,1.1));
#9443=CARTESIAN_POINT('',(-29.2842474695749,26.1117112172572,1.1));
#9444=CARTESIAN_POINT('Origin',(-28.2842474695748,26.1117112172572,0.850000000000002));
#9445=CARTESIAN_POINT('',(-29.0083854006093,26.801366389671,1.1));
#9446=CARTESIAN_POINT('Origin',(-28.2842474695748,26.1117112172572,1.1));
#9447=CARTESIAN_POINT('',(-29.0083854006093,26.801366389671,1.1));
#9448=CARTESIAN_POINT('Origin',(-26.6505694936737,28.9145730919534,0.850000000000002));
#9449=CARTESIAN_POINT('',(-27.0669231480897,28.8399017548166,1.1));
#9450=CARTESIAN_POINT('',(-26.8316039764323,29.0869868850569,1.1));
#9451=CARTESIAN_POINT('',(-27.0669231480897,28.8399017548166,1.1));
#9452=CARTESIAN_POINT('Origin',(-26.3427852170552,28.1502465824028,0.850000000000002));
#9453=CARTESIAN_POINT('',(-26.3427852170552,29.1502465824028,1.1));
#9454=CARTESIAN_POINT('Origin',(-26.3427852170552,28.1502465824028,1.1));
#9455=CARTESIAN_POINT('',(-26.3427852170552,29.1502465824028,1.1));
#9456=CARTESIAN_POINT('Origin',(-8.16563247623254,28.9002465824028,0.850000000000002));
#9457=CARTESIAN_POINT('',(-4.84975341759722,29.1502465824028,1.1));
#9458=CARTESIAN_POINT('',(-8.16563247623254,29.1502465824028,1.1));
#9459=CARTESIAN_POINT('',(-4.84975341759722,29.1502465824028,1.1));
#9460=CARTESIAN_POINT('Origin',(-4.84975341759722,25.1502465824028,0.850000000000002));
#9461=CARTESIAN_POINT('',(-0.849753417597219,25.1502465824028,1.1));
#9462=CARTESIAN_POINT('Origin',(-4.84975341759722,25.1502465824028,1.1));
#9463=CARTESIAN_POINT('',(-0.849753417597219,25.1502465824028,1.1));
#9464=CARTESIAN_POINT('Origin',(-1.09975341759722,19.7487298505949,0.85));
#9465=CARTESIAN_POINT('',(-0.849753417597219,3.65721478294476,1.1));
#9466=CARTESIAN_POINT('',(-0.849753417597219,3.65721478294476,1.1));
#9467=CARTESIAN_POINT('',(-0.849753417597219,19.7487298505949,1.1));
#9468=CARTESIAN_POINT('Origin',(-1.84975341759722,3.65721478294477,0.85));
#9469=CARTESIAN_POINT('Origin',(-1.84975341759722,3.65721478294476,1.1));
#9470=CARTESIAN_POINT('Origin',(-23.952118888438,17.1569858647893,19.));
#9471=CARTESIAN_POINT('',(-23.952118888438,10.1397931465341,7.2));
#9472=CARTESIAN_POINT('',(-23.952118888438,10.1397931465341,19.));
#9473=CARTESIAN_POINT('',(-23.952118888438,16.5670014604234,7.2));
#9474=CARTESIAN_POINT('',(-23.952118888438,15.7520994917882,7.2));
#9475=CARTESIAN_POINT('',(-23.952118888438,16.5670014604234,19.));
#9476=CARTESIAN_POINT('Origin',(-22.952118888438,10.1397931465341,19.));
#9477=CARTESIAN_POINT('',(-23.6592256696245,9.43268636534752,7.2));
#9478=CARTESIAN_POINT('',(-23.6592256696245,9.43268636534752,19.));
#9479=CARTESIAN_POINT('Origin',(-22.952118888438,10.1397931465341,7.2));
#9480=CARTESIAN_POINT('Origin',(-20.274420415839,6.04788111156204,19.));
#9481=CARTESIAN_POINT('',(-20.5673136346525,6.34077433037548,7.2));
#9482=CARTESIAN_POINT('',(-20.5673136346525,6.34077433037549,19.));
#9483=CARTESIAN_POINT('',(-20.1510261974025,5.9244868931255,7.2));
#9484=CARTESIAN_POINT('Origin',(-19.8602068534659,7.04788111156204,19.));
#9485=CARTESIAN_POINT('',(-19.8602068534659,6.04788111156203,7.2));
#9486=CARTESIAN_POINT('',(-19.8602068534659,6.04788111156204,19.));
#9487=CARTESIAN_POINT('Origin',(-19.8602068534659,7.04788111156203,7.2));
#9488=CARTESIAN_POINT('Origin',(-12.8430141352107,6.04788111156204,19.));
#9489=CARTESIAN_POINT('',(-13.4329985395765,6.04788111156203,7.2));
#9490=CARTESIAN_POINT('',(-13.4329985395765,6.04788111156204,19.));
#9491=CARTESIAN_POINT('',(-12.1622628350393,6.04788111156203,7.2));
#9492=CARTESIAN_POINT('Origin',(-13.4329985395765,7.04788111156204,19.));
#9493=CARTESIAN_POINT('',(-12.6152248047351,6.47234126185272,7.2));
#9494=CARTESIAN_POINT('',(-12.6152248047351,6.47234126185272,19.));
#9495=CARTESIAN_POINT('Origin',(-13.4329985395765,7.04788111156204,7.2));
#9496=CARTESIAN_POINT('Origin',(-10.9796773350521,5.32126156243408,19.));
#9497=CARTESIAN_POINT('',(-8.97967733505212,5.32126156243407,7.2));
#9498=CARTESIAN_POINT('',(-8.97967733505212,5.32126156243408,19.));
#9499=CARTESIAN_POINT('Origin',(-10.9796773350521,5.32126156243407,7.2));
#9500=CARTESIAN_POINT('Origin',(-8.97967733505213,3.38477775575572,19.));
#9501=CARTESIAN_POINT('',(-8.97967733505213,3.79899131812881,7.2));
#9502=CARTESIAN_POINT('',(-8.97967733505213,3.79899131812882,19.));
#9503=CARTESIAN_POINT('',(-8.97967733505213,8.86599543727138,7.2));
#9504=CARTESIAN_POINT('Origin',(-7.97967733505213,3.79899131812882,19.));
#9505=CARTESIAN_POINT('',(-8.68678411623867,3.09188453694227,7.2));
#9506=CARTESIAN_POINT('',(-8.68678411623867,3.09188453694227,19.));
#9507=CARTESIAN_POINT('Origin',(-7.97967733505213,3.79899131812881,7.2));
#9508=CARTESIAN_POINT('Origin',(-6.31065210972155,0.715752530425147,19.));
#9509=CARTESIAN_POINT('',(-6.603545328535,1.00864574923859,7.2));
#9510=CARTESIAN_POINT('',(-6.603545328535,1.0086457492386,19.));
#9511=CARTESIAN_POINT('',(-11.0112321130986,5.4163325338022,7.2));
#9512=CARTESIAN_POINT('Origin',(-5.89643854734845,1.71575253042514,19.));
#9513=CARTESIAN_POINT('',(-5.89643854734845,0.715752530425142,7.2));
#9514=CARTESIAN_POINT('',(-5.89643854734845,0.715752530425147,19.));
#9515=CARTESIAN_POINT('Origin',(-5.89643854734845,1.71575253042514,7.2));
#9516=CARTESIAN_POINT('Origin',(-3.48828878274281,0.715752530425147,19.));
#9517=CARTESIAN_POINT('',(-3.88828878274281,0.715752530425142,7.2));
#9518=CARTESIAN_POINT('',(-3.88828878274281,0.715752530425147,19.));
#9519=CARTESIAN_POINT('',(-7.48490015880533,0.715752530425142,7.2));
#9520=CARTESIAN_POINT('Origin',(-3.88828878274281,1.71575253042515,19.));
#9521=CARTESIAN_POINT('',(-3.19863361032902,0.99161459939066,7.2));
#9522=CARTESIAN_POINT('',(-3.19863361032902,0.991614599390664,19.));
#9523=CARTESIAN_POINT('Origin',(-3.88828878274281,1.71575253042514,7.2));
#9524=CARTESIAN_POINT('Origin',(-0.849753417597219,3.22864335437334,19.));
#9525=CARTESIAN_POINT('',(-1.16009824518343,2.93307685191027,7.2));
#9526=CARTESIAN_POINT('',(-1.16009824518343,2.93307685191028,19.));
#9527=CARTESIAN_POINT('',(-0.860934171855592,3.21799501698441,7.2));
#9528=CARTESIAN_POINT('Origin',(-1.03334796495904,3.39902949974302,7.45));
#9529=CARTESIAN_POINT('',(-3.54346119653592,1.3536835649079,7.69999999999999));
#9530=CARTESIAN_POINT('',(-1.16009824518343,2.93307685191027,7.2));
#9531=CARTESIAN_POINT('Origin',(-3.88828878274281,1.71575253042514,7.44999999999999));
#9532=CARTESIAN_POINT('',(-3.88828878274281,1.21575253042514,7.69999999999999));
#9533=CARTESIAN_POINT('Origin',(-7.48490015880533,0.965752530425141,7.44999999999999));
#9534=CARTESIAN_POINT('',(-5.89643854734845,1.21575253042514,7.69999999999999));
#9535=CARTESIAN_POINT('Origin',(-5.89643854734845,1.71575253042514,7.44999999999999));
#9536=CARTESIAN_POINT('',(-6.24999193794173,1.36219913983186,7.69999999999999));
#9537=CARTESIAN_POINT('Origin',(-10.834455417802,5.59310922909884,7.45));
#9538=CARTESIAN_POINT('',(-8.3332307256454,3.44543792753554,7.7));
#9539=CARTESIAN_POINT('Origin',(-7.97967733505213,3.79899131812881,7.45));
#9540=CARTESIAN_POINT('',(-8.47967733505213,3.79899131812881,7.7));
#9541=CARTESIAN_POINT('Origin',(-8.72967733505213,8.86599543727138,7.45));
#9542=CARTESIAN_POINT('',(-8.47967733505213,5.32126156243407,7.7));
#9543=CARTESIAN_POINT('Origin',(-10.9796773350521,5.32126156243407,7.45));
#9544=CARTESIAN_POINT('',(-13.0241116721558,6.76011118670738,7.7));
#9545=CARTESIAN_POINT('Origin',(-13.4329985395765,7.04788111156204,7.45));
#9546=CARTESIAN_POINT('',(-13.4329985395765,6.54788111156204,7.7));
#9547=CARTESIAN_POINT('Origin',(-12.1622628350393,6.29788111156203,7.45));
#9548=CARTESIAN_POINT('',(-19.8602068534659,6.54788111156203,7.7));
#9549=CARTESIAN_POINT('Origin',(-19.8602068534659,7.04788111156203,7.45));
#9550=CARTESIAN_POINT('',(-20.2137602440592,6.69432772096875,7.7));
#9551=CARTESIAN_POINT('Origin',(-19.9742495021059,6.10126358842214,7.45));
#9552=CARTESIAN_POINT('',(-23.3056722790312,9.78623975594079,7.7));
#9553=CARTESIAN_POINT('Origin',(-22.952118888438,10.1397931465341,7.45));
#9554=CARTESIAN_POINT('',(-23.452118888438,10.1397931465341,7.7));
#9555=CARTESIAN_POINT('Origin',(-23.702118888438,15.7520994917882,7.45));
#9556=CARTESIAN_POINT('',(-23.452118888438,16.5670014604234,7.7));
#9557=CARTESIAN_POINT('Origin',(-22.952118888438,16.5670014604234,7.45));
#9558=CARTESIAN_POINT('',(-23.5276587381473,17.3847751952649,7.2));
#9559=CARTESIAN_POINT('',(-23.2398888132926,16.9758883278442,7.7));
#9560=CARTESIAN_POINT('Origin',(-22.952118888438,16.5670014604234,7.2));
#9561=CARTESIAN_POINT('Origin',(-24.6787384375659,19.0203226649479,7.45));
#9562=CARTESIAN_POINT('',(-24.6787384375659,21.0203226649479,7.2));
#9563=CARTESIAN_POINT('',(-24.6787384375659,21.5203226649479,7.7));
#9564=CARTESIAN_POINT('Origin',(-24.6787384375659,19.0203226649479,7.2));
#9565=CARTESIAN_POINT('Origin',(-19.0483668895561,21.2703226649479,7.45));
#9566=CARTESIAN_POINT('',(-26.2010086818712,21.0203226649479,7.2));
#9567=CARTESIAN_POINT('',(-26.2010086818712,21.5203226649479,7.7));
#9568=CARTESIAN_POINT('',(-19.0483668895561,21.0203226649479,7.2));
#9569=CARTESIAN_POINT('Origin',(-26.2010086818712,22.0203226649479,7.45));
#9570=CARTESIAN_POINT('',(-26.9081154630577,21.3132158837613,7.2));
#9571=CARTESIAN_POINT('',(-26.5545620724644,21.6667692743546,7.7));
#9572=CARTESIAN_POINT('Origin',(-26.2010086818712,22.0203226649479,7.2));
#9573=CARTESIAN_POINT('Origin',(-22.3212530977286,17.0799069090255,7.45));
#9574=CARTESIAN_POINT('',(-28.9913542507614,23.396454671465,7.2));
#9575=CARTESIAN_POINT('',(-28.6378008601681,23.7500080620583,7.7));
#9576=CARTESIAN_POINT('',(-22.4980297930252,16.9031302137289,7.2));
#9577=CARTESIAN_POINT('Origin',(-28.2842474695748,24.1035614526515,7.45));
#9578=CARTESIAN_POINT('',(-29.2842474695749,24.1035614526515,7.2));
#9579=CARTESIAN_POINT('',(-28.7842474695749,24.1035614526515,7.7));
#9580=CARTESIAN_POINT('Origin',(-28.2842474695748,24.1035614526515,7.2));
#9581=CARTESIAN_POINT('Origin',(-29.0342474695749,20.4294621680221,7.45));
#9582=CARTESIAN_POINT('',(-29.2842474695749,26.1117112172572,7.2));
#9583=CARTESIAN_POINT('',(-28.7842474695749,26.1117112172572,7.7));
#9584=CARTESIAN_POINT('',(-29.2842474695749,20.4294621680221,7.2));
#9585=CARTESIAN_POINT('Origin',(-28.2842474695748,26.1117112172572,7.45));
#9586=CARTESIAN_POINT('',(-29.0083854006093,26.801366389671,7.2));
#9587=CARTESIAN_POINT('',(-28.6463164350921,26.4565388034641,7.7));
#9588=CARTESIAN_POINT('Origin',(-28.2842474695748,26.1117112172572,7.2));
#9589=CARTESIAN_POINT('Origin',(-26.6505694936737,28.9145730919534,7.45));
#9590=CARTESIAN_POINT('',(-27.0669231480897,28.8399017548166,7.2));
#9591=CARTESIAN_POINT('',(-26.7048541825725,28.4950741686097,7.7));
#9592=CARTESIAN_POINT('',(-26.8316039764323,29.0869868850569,7.2));
#9593=CARTESIAN_POINT('Origin',(-26.3427852170552,28.1502465824028,7.45));
#9594=CARTESIAN_POINT('',(-26.3427852170552,29.1502465824028,7.2));
#9595=CARTESIAN_POINT('',(-26.3427852170552,28.6502465824028,7.7));
#9596=CARTESIAN_POINT('Origin',(-26.3427852170552,28.1502465824028,7.2));
#9597=CARTESIAN_POINT('Origin',(-8.16563247623254,28.9002465824028,7.45));
#9598=CARTESIAN_POINT('',(-4.84975341759722,29.1502465824028,7.2));
#9599=CARTESIAN_POINT('',(-4.84975341759722,28.6502465824028,7.7));
#9600=CARTESIAN_POINT('',(-8.16563247623254,29.1502465824028,7.2));
#9601=CARTESIAN_POINT('Origin',(-4.84975341759722,25.1502465824028,7.45));
#9602=CARTESIAN_POINT('',(-0.849753417597219,25.1502465824028,7.2));
#9603=CARTESIAN_POINT('',(-1.34975341759722,25.1502465824028,7.7));
#9604=CARTESIAN_POINT('Origin',(-4.84975341759722,25.1502465824028,7.2));
#9605=CARTESIAN_POINT('Origin',(-1.09975341759722,19.7487298505949,7.45));
#9606=CARTESIAN_POINT('',(-0.849753417597219,3.65721478294476,7.2));
#9607=CARTESIAN_POINT('',(-1.34975341759722,3.65721478294476,7.7));
#9608=CARTESIAN_POINT('',(-0.849753417597219,19.7487298505949,7.2));
#9609=CARTESIAN_POINT('Origin',(-1.84975341759722,3.65721478294476,7.45));
#9610=CARTESIAN_POINT('Origin',(-1.84975341759722,3.65721478294476,7.2));
#9611=CARTESIAN_POINT('Origin',(-24.6787384375659,19.0203226649479,19.));
#9612=CARTESIAN_POINT('',(-23.5276587381473,17.3847751952649,19.));
#9613=CARTESIAN_POINT('',(-24.6787384375659,21.0203226649479,19.));
#9614=CARTESIAN_POINT('Origin',(-26.6152222442443,21.0203226649479,19.));
#9615=CARTESIAN_POINT('',(-26.2010086818712,21.0203226649479,19.));
#9616=CARTESIAN_POINT('Origin',(-26.2010086818712,22.0203226649479,19.));
#9617=CARTESIAN_POINT('',(-26.9081154630577,21.3132158837613,19.));
#9618=CARTESIAN_POINT('Origin',(-29.2842474695749,23.6893478902784,19.));
#9619=CARTESIAN_POINT('',(-28.9913542507614,23.396454671465,19.));
#9620=CARTESIAN_POINT('Origin',(-28.2842474695748,24.1035614526515,19.));
#9621=CARTESIAN_POINT('',(-29.2842474695749,24.1035614526515,19.));
#9622=CARTESIAN_POINT('Origin',(-29.2842474695749,26.5117112172572,19.));
#9623=CARTESIAN_POINT('',(-29.2842474695749,26.1117112172572,19.));
#9624=CARTESIAN_POINT('Origin',(-28.2842474695748,26.1117112172572,19.));
#9625=CARTESIAN_POINT('',(-29.0083854006093,26.801366389671,19.));
#9626=CARTESIAN_POINT('Origin',(-26.7713566456267,29.1502465824028,19.));
#9627=CARTESIAN_POINT('',(-27.0669231480897,28.8399017548166,19.));
#9628=CARTESIAN_POINT('Origin',(-26.3427852170552,28.1502465824028,19.));
#9629=CARTESIAN_POINT('',(-26.3427852170552,29.1502465824028,19.));
#9630=CARTESIAN_POINT('Origin',(-4.84975341759722,29.1502465824028,19.));
#9631=CARTESIAN_POINT('',(-4.84975341759722,29.1502465824028,19.));
#9632=CARTESIAN_POINT('Origin',(-4.84975341759722,25.1502465824028,19.));
#9633=CARTESIAN_POINT('',(-0.849753417597219,25.1502465824028,19.));
#9634=CARTESIAN_POINT('Origin',(-0.849753417597219,25.1502465824028,19.));
#9635=CARTESIAN_POINT('',(-0.849753417597219,3.65721478294476,19.));
#9636=CARTESIAN_POINT('Origin',(-1.84975341759722,3.65721478294476,19.));
#9637=CARTESIAN_POINT('Origin',(-22.952118888438,16.5670014604234,19.));
#9638=CARTESIAN_POINT('Origin',(-14.801482994706,15.198517005294,19.));
#9639=CARTESIAN_POINT('',(-20.801482994706,15.198517005294,19.));
#11361=UNCERTAINTY_MEASURE_WITH_UNIT(LENGTH_MEASURE(0.01),#11386,
'DISTANCE_ACCURACY_VALUE',
'Maximum model space distance between geometric entities at asserted c
onnectivities');
#11370=UNCERTAINTY_MEASURE_WITH_UNIT(LENGTH_MEASURE(0.01),#11386,
'DISTANCE_ACCURACY_VALUE',
'Maximum model space distance between geometric entities at asserted c
onnectivities');
#11376=(
GEOMETRIC_REPRESENTATION_CONTEXT(3)
GLOBAL_UNCERTAINTY_ASSIGNED_CONTEXT((#11361))
GLOBAL_UNIT_ASSIGNED_CONTEXT((#11386,#11388,#11389))
REPRESENTATION_CONTEXT('','3D')
);
#11385=(
GEOMETRIC_REPRESENTATION_CONTEXT(3)
GLOBAL_UNCERTAINTY_ASSIGNED_CONTEXT((#11370))
GLOBAL_UNIT_ASSIGNED_CONTEXT((#11386,#11388,#11389))
REPRESENTATION_CONTEXT('','3D')
);
#11386=(
LENGTH_UNIT()
NAMED_UNIT(*)
SI_UNIT(.MILLI.,.METRE.)
);
#11388=(
NAMED_UNIT(*)
PLANE_ANGLE_UNIT()
SI_UNIT($,.RADIAN.)
);
#11389=(
NAMED_UNIT(*)
SI_UNIT($,.STERADIAN.)
SOLID_ANGLE_UNIT()
);
#11395=SHAPE_DEFINITION_REPRESENTATION(#11409,#11436);
#11409=PRODUCT_DEFINITION_SHAPE('',$,#11451);
#11436=SHAPE_REPRESENTATION('',(#5817),#11376);
#11445=PRODUCT_DEFINITION_CONTEXT('part definition',#11489,'design');
#11451=PRODUCT_DEFINITION('Bottom_Block','Bottom_Block',#11465,#11445);
#11465=PRODUCT_DEFINITION_FORMATION('',$,#11496);
#11489=APPLICATION_CONTEXT(
'Core Data for Automotive Mechanical Design Process');
#11490=PRODUCT_CONTEXT('part definition',#11489,'mechanical');
#11496=PRODUCT('Bottom_Block','Bottom_Block',$,(#11490));
#11540=COLOUR_RGB('Dark Blue',0.08,0.2,0.34);
#11541=FILL_AREA_STYLE_COLOUR('',#11540);
#11542=FILL_AREA_STYLE('',(#11541));
#11543=SURFACE_STYLE_FILL_AREA(#11542);
#11544=SURFACE_SIDE_STYLE('',(#11543));
#11545=SURFACE_STYLE_USAGE(.BOTH.,#11544);
#11546=PRESENTATION_STYLE_ASSIGNMENT((#11545));
ENDSEC;
END-ISO-10303-21;
